ISO-10303-21;
HEADER;
/* Generated by software containing ST-Developer
 * from STEP Tools, Inc. (www.steptools.com) 
 */

FILE_DESCRIPTION(
/* description */ ('STEP AP214'),
/* implementation_level */ '2;1');

FILE_NAME(
/* name */ 'PUR-HW-4007.step',
/* time_stamp */ '2026-10-07T12:49:37-07:00',
/* author */ (''),
/* organization */ (''),
/* preprocessor_version */ 'ST-DEVELOPER v20.2',
/* originating_system */ 'Autodesk Translation Framework v15.15.0.0',
/* authorisation */ '');

FILE_SCHEMA (('AUTOMOTIVE_DESIGN { 1 0 10303 214 3 1 1 }'));
ENDSEC;

DATA;
#10=MECHANICAL_DESIGN_GEOMETRIC_PRESENTATION_REPRESENTATION('',(#292),#33016);
#190=(
BOUNDED_CURVE()
B_SPLINE_CURVE(2,(#18409,#18410,#18411,#18412,#18413,#18414,#18415,#18416,
#18417,#18418,#18419,#18420,#18421),.UNSPECIFIED.,.F.,.F.)
B_SPLINE_CURVE_WITH_KNOTS((3,2,2,2,2,2,3),(0.833333333333333,0.861111111111111,
0.888888888888889,0.916666666666667,0.944444444444444,0.972222222222222,
1.),.UNSPECIFIED.)
CURVE()
GEOMETRIC_REPRESENTATION_ITEM()
RATIONAL_B_SPLINE_CURVE((1.,0.866025403784439,1.,0.866025403784439,1.,0.866025403784439,
1.,0.866025403784439,1.,0.866025403784439,1.,0.866025403784439,1.))
REPRESENTATION_ITEM('')
);
#191=(
BOUNDED_CURVE()
B_SPLINE_CURVE(2,(#18423,#18424,#18425,#18426,#18427,#18428,#18429,#18430,
#18431,#18432,#18433,#18434,#18435,#18436,#18437,#18438,#18439,#18440,#18441,
#18442,#18443,#18444,#18445,#18446,#18447,#18448,#18449,#18450,#18451,#18452,
#18453,#18454,#18455,#18456,#18457,#18458,#18459,#18460,#18461,#18462,#18463,
#18464,#18465,#18466,#18467,#18468,#18469,#18470,#18471,#18472,#18473,#18474,
#18475,#18476,#18477,#18478,#18479,#18480,#18481,#18482,#18483),
 .UNSPECIFIED.,.F.,.F.)
B_SPLINE_CURVE_WITH_KNOTS((3,2,2,2,2,2,2,2,2,2,2,2,2,2,2,2,2,2,2,2,2,2,
2,2,2,2,2,2,2,2,3),(0.,0.0277777777777778,0.0555555555555556,0.0833333333333333,
0.111111111111111,0.138888888888889,0.166666666666667,0.194444444444444,
0.222222222222222,0.25,0.277777777777778,0.305555555555556,0.333333333333333,
0.361111111111111,0.388888888888889,0.416666666666667,0.444444444444444,
0.472222222222222,0.5,0.527777777777778,0.555555555555556,0.583333333333333,
0.611111111111111,0.638888888888889,0.666666666666667,0.694444444444444,
0.722222222222222,0.75,0.777777777777778,0.805555555555556,0.833333333333333),
 .UNSPECIFIED.)
CURVE()
GEOMETRIC_REPRESENTATION_ITEM()
RATIONAL_B_SPLINE_CURVE((1.,0.866025403784439,1.,0.866025403784439,1.,0.866025403784439,
1.,0.866025403784439,1.,0.866025403784439,1.,0.866025403784439,1.,0.866025403784439,
1.,0.866025403784439,1.,0.866025403784439,1.,0.866025403784439,1.,0.866025403784439,
1.,0.866025403784439,1.,0.866025403784439,1.,0.866025403784439,1.,0.866025403784439,
1.,0.866025403784439,1.,0.866025403784439,1.,0.866025403784439,1.,0.866025403784439,
1.,0.866025403784439,1.,0.866025403784439,1.,0.866025403784439,1.,0.866025403784439,
1.,0.866025403784439,1.,0.866025403784439,1.,0.866025403784439,1.,0.866025403784439,
1.,0.866025403784439,1.,0.866025403784439,1.,0.866025403784439,1.))
REPRESENTATION_ITEM('')
);
#192=(
BOUNDED_CURVE()
B_SPLINE_CURVE(2,(#18486,#18487,#18488,#18489,#18490,#18491,#18492,#18493,
#18494,#18495,#18496,#18497,#18498,#18499,#18500,#18501,#18502,#18503,#18504,
#18505,#18506,#18507,#18508,#18509,#18510,#18511,#18512,#18513,#18514,#18515,
#18516,#18517,#18518,#18519,#18520,#18521,#18522,#18523,#18524,#18525,#18526,
#18527,#18528,#18529,#18530,#18531,#18532,#18533,#18534,#18535,#18536,#18537,
#18538,#18539,#18540,#18541,#18542,#18543,#18544,#18545,#18546,#18547,#18548,
#18549,#18550,#18551,#18552,#18553,#18554,#18555,#18556,#18557,#18558),
 .UNSPECIFIED.,.F.,.F.)
B_SPLINE_CURVE_WITH_KNOTS((3,2,2,2,2,2,2,2,2,2,2,2,2,2,2,2,2,2,2,2,2,2,
2,2,2,2,2,2,2,2,2,2,2,2,2,2,3),(0.,0.0277777777777778,0.0555555555555556,
0.0833333333333333,0.111111111111111,0.138888888888889,0.166666666666667,
0.194444444444444,0.222222222222222,0.25,0.277777777777778,0.305555555555556,
0.333333333333333,0.361111111111111,0.388888888888889,0.416666666666667,
0.444444444444444,0.472222222222222,0.5,0.527777777777778,0.555555555555556,
0.583333333333333,0.611111111111111,0.638888888888889,0.666666666666667,
0.694444444444444,0.722222222222222,0.75,0.777777777777778,0.805555555555556,
0.833333333333333,0.861111111111111,0.888888888888889,0.916666666666667,
0.944444444444444,0.972222222222222,1.),.UNSPECIFIED.)
CURVE()
GEOMETRIC_REPRESENTATION_ITEM()
RATIONAL_B_SPLINE_CURVE((1.,0.866025403784439,1.,0.866025403784439,1.,0.866025403784439,
1.,0.866025403784439,1.,0.866025403784439,1.,0.866025403784439,1.,0.866025403784439,
1.,0.866025403784439,1.,0.866025403784439,1.,0.866025403784439,1.,0.866025403784439,
1.,0.866025403784439,1.,0.866025403784439,1.,0.866025403784439,1.,0.866025403784439,
1.,0.866025403784439,1.,0.866025403784439,1.,0.866025403784439,1.,0.866025403784439,
1.,0.866025403784439,1.,0.866025403784439,1.,0.866025403784439,1.,0.866025403784439,
1.,0.866025403784439,1.,0.866025403784439,1.,0.866025403784439,1.,0.866025403784439,
1.,0.866025403784439,1.,0.866025403784439,1.,0.866025403784439,1.,0.866025403784439,
1.,0.866025403784439,1.,0.866025403784439,1.,0.866025403784439,1.,0.866025403784439,
1.,0.866025403784439,1.))
REPRESENTATION_ITEM('')
);
#193=(
BOUNDED_CURVE()
B_SPLINE_CURVE(2,(#18853,#18854,#18855,#18856,#18857,#18858,#18859,#18860,
#18861,#18862,#18863,#18864,#18865),.UNSPECIFIED.,.F.,.F.)
B_SPLINE_CURVE_WITH_KNOTS((3,2,2,2,2,2,3),(0.,0.0277777777777778,0.0555555555555556,
0.0833333333333333,0.111111111111111,0.138888888888889,0.166666666666667),
 .UNSPECIFIED.)
CURVE()
GEOMETRIC_REPRESENTATION_ITEM()
RATIONAL_B_SPLINE_CURVE((1.,0.866025403784439,1.,0.866025403784439,1.,0.866025403784439,
1.,0.866025403784439,1.,0.866025403784439,1.,0.866025403784439,1.))
REPRESENTATION_ITEM('')
);
#194=(
BOUNDED_CURVE()
B_SPLINE_CURVE(2,(#18866,#18867,#18868,#18869,#18870,#18871,#18872,#18873,
#18874,#18875,#18876,#18877,#18878,#18879,#18880,#18881,#18882,#18883,#18884,
#18885,#18886,#18887,#18888,#18889,#18890,#18891,#18892,#18893,#18894,#18895,
#18896,#18897,#18898,#18899,#18900,#18901,#18902,#18903,#18904,#18905,#18906,
#18907,#18908,#18909,#18910,#18911,#18912,#18913,#18914,#18915,#18916,#18917,
#18918,#18919,#18920,#18921,#18922,#18923,#18924,#18925,#18926),
 .UNSPECIFIED.,.F.,.F.)
B_SPLINE_CURVE_WITH_KNOTS((3,2,2,2,2,2,2,2,2,2,2,2,2,2,2,2,2,2,2,2,2,2,
2,2,2,2,2,2,2,2,3),(0.,0.0277777777777778,0.0555555555555556,0.0833333333333333,
0.111111111111111,0.138888888888889,0.166666666666667,0.194444444444444,
0.222222222222222,0.25,0.277777777777778,0.305555555555556,0.333333333333333,
0.361111111111111,0.388888888888889,0.416666666666667,0.444444444444444,
0.472222222222222,0.5,0.527777777777778,0.555555555555556,0.583333333333333,
0.611111111111111,0.638888888888889,0.666666666666667,0.694444444444444,
0.722222222222222,0.75,0.777777777777778,0.805555555555556,0.833333333333333),
 .UNSPECIFIED.)
CURVE()
GEOMETRIC_REPRESENTATION_ITEM()
RATIONAL_B_SPLINE_CURVE((1.,0.866025403784439,1.,0.866025403784439,1.,0.866025403784439,
1.,0.866025403784439,1.,0.866025403784439,1.,0.866025403784439,1.,0.866025403784439,
1.,0.866025403784439,1.,0.866025403784439,1.,0.866025403784439,1.,0.866025403784439,
1.,0.866025403784439,1.,0.866025403784439,1.,0.866025403784439,1.,0.866025403784439,
1.,0.866025403784439,1.,0.866025403784439,1.,0.866025403784439,1.,0.866025403784439,
1.,0.866025403784439,1.,0.866025403784439,1.,0.866025403784439,1.,0.866025403784439,
1.,0.866025403784439,1.,0.866025403784439,1.,0.866025403784439,1.,0.866025403784439,
1.,0.866025403784439,1.,0.866025403784439,1.,0.866025403784439,1.))
REPRESENTATION_ITEM('')
);
#195=(
BOUNDED_CURVE()
B_SPLINE_CURVE(2,(#19223,#19224,#19225,#19226,#19227,#19228,#19229,#19230,
#19231,#19232,#19233,#19234,#19235,#19236,#19237,#19238,#19239,#19240,#19241,
#19242,#19243,#19244,#19245,#19246,#19247,#19248,#19249,#19250,#19251,#19252,
#19253,#19254,#19255,#19256,#19257,#19258,#19259,#19260,#19261,#19262,#19263,
#19264,#19265,#19266,#19267,#19268,#19269,#19270,#19271,#19272,#19273,#19274,
#19275,#19276,#19277,#19278,#19279,#19280,#19281,#19282,#19283,#19284,#19285,
#19286,#19287,#19288,#19289,#19290,#19291,#19292,#19293,#19294,#19295),
 .UNSPECIFIED.,.F.,.F.)
B_SPLINE_CURVE_WITH_KNOTS((3,2,2,2,2,2,2,2,2,2,2,2,2,2,2,2,2,2,2,2,2,2,
2,2,2,2,2,2,2,2,2,2,2,2,2,2,3),(0.,0.0277777777777778,0.0555555555555556,
0.0833333333333333,0.111111111111111,0.138888888888889,0.166666666666667,
0.194444444444444,0.222222222222222,0.25,0.277777777777778,0.305555555555556,
0.333333333333333,0.361111111111111,0.388888888888889,0.416666666666667,
0.444444444444444,0.472222222222222,0.5,0.527777777777778,0.555555555555556,
0.583333333333333,0.611111111111111,0.638888888888889,0.666666666666667,
0.694444444444444,0.722222222222222,0.75,0.777777777777778,0.805555555555556,
0.833333333333333,0.861111111111111,0.888888888888889,0.916666666666667,
0.944444444444444,0.972222222222222,1.),.UNSPECIFIED.)
CURVE()
GEOMETRIC_REPRESENTATION_ITEM()
RATIONAL_B_SPLINE_CURVE((1.,0.866025403784439,1.,0.866025403784439,1.,0.866025403784439,
1.,0.866025403784439,1.,0.866025403784439,1.,0.866025403784439,1.,0.866025403784439,
1.,0.866025403784439,1.,0.866025403784439,1.,0.866025403784439,1.,0.866025403784439,
1.,0.866025403784439,1.,0.866025403784439,1.,0.866025403784439,1.,0.866025403784439,
1.,0.866025403784439,1.,0.866025403784439,1.,0.866025403784439,1.,0.866025403784439,
1.,0.866025403784439,1.,0.866025403784439,1.,0.866025403784439,1.,0.866025403784439,
1.,0.866025403784439,1.,0.866025403784439,1.,0.866025403784439,1.,0.866025403784439,
1.,0.866025403784439,1.,0.866025403784439,1.,0.866025403784439,1.,0.866025403784439,
1.,0.866025403784439,1.,0.866025403784439,1.,0.866025403784439,1.,0.866025403784439,
1.,0.866025403784439,1.))
REPRESENTATION_ITEM('')
);
#238=SHAPE_REPRESENTATION_RELATIONSHIP('SRR','None',#33131,#265);
#265=ADVANCED_BREP_SHAPE_REPRESENTATION('',(#323),#32992);
#292=STYLED_ITEM('',(#33285),#323);
#323=MANIFOLD_SOLID_BREP('Body1',#9947);
#431=(
BOUNDED_SURFACE()
B_SPLINE_SURFACE(3,2,((#18113,#18114,#18115,#18116,#18117,#18118,#18119,
#18120,#18121,#18122,#18123,#18124,#18125,#18126,#18127,#18128,#18129,#18130,
#18131,#18132,#18133,#18134,#18135,#18136,#18137,#18138,#18139,#18140,#18141,
#18142,#18143,#18144,#18145,#18146,#18147,#18148,#18149,#18150,#18151,#18152,
#18153,#18154,#18155,#18156,#18157,#18158,#18159,#18160,#18161,#18162,#18163,
#18164,#18165,#18166,#18167,#18168,#18169,#18170,#18171,#18172,#18173,#18174,
#18175,#18176,#18177,#18178,#18179,#18180,#18181,#18182,#18183,#18184,#18185),
(#18186,#18187,#18188,#18189,#18190,#18191,#18192,#18193,#18194,#18195,
#18196,#18197,#18198,#18199,#18200,#18201,#18202,#18203,#18204,#18205,#18206,
#18207,#18208,#18209,#18210,#18211,#18212,#18213,#18214,#18215,#18216,#18217,
#18218,#18219,#18220,#18221,#18222,#18223,#18224,#18225,#18226,#18227,#18228,
#18229,#18230,#18231,#18232,#18233,#18234,#18235,#18236,#18237,#18238,#18239,
#18240,#18241,#18242,#18243,#18244,#18245,#18246,#18247,#18248,#18249,#18250,
#18251,#18252,#18253,#18254,#18255,#18256,#18257,#18258),(#18259,#18260,
#18261,#18262,#18263,#18264,#18265,#18266,#18267,#18268,#18269,#18270,#18271,
#18272,#18273,#18274,#18275,#18276,#18277,#18278,#18279,#18280,#18281,#18282,
#18283,#18284,#18285,#18286,#18287,#18288,#18289,#18290,#18291,#18292,#18293,
#18294,#18295,#18296,#18297,#18298,#18299,#18300,#18301,#18302,#18303,#18304,
#18305,#18306,#18307,#18308,#18309,#18310,#18311,#18312,#18313,#18314,#18315,
#18316,#18317,#18318,#18319,#18320,#18321,#18322,#18323,#18324,#18325,#18326,
#18327,#18328,#18329,#18330,#18331),(#18332,#18333,#18334,#18335,#18336,
#18337,#18338,#18339,#18340,#18341,#18342,#18343,#18344,#18345,#18346,#18347,
#18348,#18349,#18350,#18351,#18352,#18353,#18354,#18355,#18356,#18357,#18358,
#18359,#18360,#18361,#18362,#18363,#18364,#18365,#18366,#18367,#18368,#18369,
#18370,#18371,#18372,#18373,#18374,#18375,#18376,#18377,#18378,#18379,#18380,
#18381,#18382,#18383,#18384,#18385,#18386,#18387,#18388,#18389,#18390,#18391,
#18392,#18393,#18394,#18395,#18396,#18397,#18398,#18399,#18400,#18401,#18402,
#18403,#18404)),.UNSPECIFIED.,.F.,.F.,.F.)
B_SPLINE_SURFACE_WITH_KNOTS((4,4),(3,2,2,2,2,2,2,2,2,2,2,2,2,2,2,2,2,2,
2,2,2,2,2,2,2,2,2,2,2,2,2,2,2,2,2,2,3),(0.,1.),(0.,0.0277777777777778,0.0555555555555556,
0.0833333333333333,0.111111111111111,0.138888888888889,0.166666666666667,
0.194444444444444,0.222222222222222,0.25,0.277777777777778,0.305555555555556,
0.333333333333333,0.361111111111111,0.388888888888889,0.416666666666667,
0.444444444444444,0.472222222222222,0.5,0.527777777777778,0.555555555555556,
0.583333333333333,0.611111111111111,0.638888888888889,0.666666666666667,
0.694444444444444,0.722222222222222,0.75,0.777777777777778,0.805555555555556,
0.833333333333333,0.861111111111111,0.888888888888889,0.916666666666667,
0.944444444444444,0.972222222222222,1.),.UNSPECIFIED.)
GEOMETRIC_REPRESENTATION_ITEM()
RATIONAL_B_SPLINE_SURFACE(((1.,0.866025403784439,1.,0.866025403784439,1.,
0.866025403784439,1.,0.866025403784439,1.,0.866025403784439,1.,0.866025403784439,
1.,0.866025403784439,1.,0.866025403784439,1.,0.866025403784439,1.,0.866025403784439,
1.,0.866025403784439,1.,0.866025403784439,1.,0.866025403784439,1.,0.866025403784439,
1.,0.866025403784439,1.,0.866025403784439,1.,0.866025403784439,1.,0.866025403784439,
1.,0.866025403784439,1.,0.866025403784439,1.,0.866025403784439,1.,0.866025403784439,
1.,0.866025403784439,1.,0.866025403784439,1.,0.866025403784439,1.,0.866025403784439,
1.,0.866025403784439,1.,0.866025403784439,1.,0.866025403784439,1.,0.866025403784439,
1.,0.866025403784439,1.,0.866025403784439,1.,0.866025403784439,1.,0.866025403784439,
1.,0.866025403784439,1.,0.866025403784439,1.),(0.804737854124365,0.696923425058676,
0.804737854124365,0.696923425058676,0.804737854124365,0.696923425058676,
0.804737854124365,0.696923425058676,0.804737854124365,0.696923425058676,
0.804737854124365,0.696923425058676,0.804737854124365,0.696923425058676,
0.804737854124365,0.696923425058676,0.804737854124365,0.696923425058676,
0.804737854124365,0.696923425058676,0.804737854124365,0.696923425058676,
0.804737854124365,0.696923425058676,0.804737854124365,0.696923425058676,
0.804737854124365,0.696923425058676,0.804737854124365,0.696923425058676,
0.804737854124365,0.696923425058676,0.804737854124365,0.696923425058676,
0.804737854124365,0.696923425058676,0.804737854124365,0.696923425058676,
0.804737854124365,0.696923425058676,0.804737854124365,0.696923425058676,
0.804737854124365,0.696923425058676,0.804737854124365,0.696923425058676,
0.804737854124365,0.696923425058676,0.804737854124365,0.696923425058676,
0.804737854124365,0.696923425058676,0.804737854124365,0.696923425058676,
0.804737854124365,0.696923425058676,0.804737854124365,0.696923425058676,
0.804737854124365,0.696923425058676,0.804737854124365,0.696923425058676,
0.804737854124365,0.696923425058676,0.804737854124365,0.696923425058676,
0.804737854124365,0.696923425058676,0.804737854124365,0.696923425058676,
0.804737854124365,0.696923425058676,0.804737854124365),(0.804737854124365,
0.696923425058676,0.804737854124365,0.696923425058676,0.804737854124365,
0.696923425058676,0.804737854124365,0.696923425058676,0.804737854124365,
0.696923425058676,0.804737854124365,0.696923425058676,0.804737854124365,
0.696923425058676,0.804737854124365,0.696923425058676,0.804737854124365,
0.696923425058676,0.804737854124365,0.696923425058676,0.804737854124365,
0.696923425058676,0.804737854124365,0.696923425058676,0.804737854124365,
0.696923425058676,0.804737854124365,0.696923425058676,0.804737854124365,
0.696923425058676,0.804737854124365,0.696923425058676,0.804737854124365,
0.696923425058676,0.804737854124365,0.696923425058676,0.804737854124365,
0.696923425058676,0.804737854124365,0.696923425058676,0.804737854124365,
0.696923425058676,0.804737854124365,0.696923425058676,0.804737854124365,
0.696923425058676,0.804737854124365,0.696923425058676,0.804737854124365,
0.696923425058676,0.804737854124365,0.696923425058676,0.804737854124365,
0.696923425058676,0.804737854124365,0.696923425058676,0.804737854124365,
0.696923425058676,0.804737854124365,0.696923425058676,0.804737854124365,
0.696923425058676,0.804737854124365,0.696923425058676,0.804737854124365,
0.696923425058676,0.804737854124365,0.696923425058676,0.804737854124365,
0.696923425058676,0.804737854124365,0.696923425058676,0.804737854124365),
(1.,0.866025403784439,1.,0.866025403784439,1.,0.866025403784439,1.,0.866025403784439,
1.,0.866025403784439,1.,0.866025403784439,1.,0.866025403784439,1.,0.866025403784439,
1.,0.866025403784439,1.,0.866025403784439,1.,0.866025403784439,1.,0.866025403784439,
1.,0.866025403784439,1.,0.866025403784439,1.,0.866025403784439,1.,0.866025403784439,
1.,0.866025403784439,1.,0.866025403784439,1.,0.866025403784439,1.,0.866025403784439,
1.,0.866025403784439,1.,0.866025403784439,1.,0.866025403784439,1.,0.866025403784439,
1.,0.866025403784439,1.,0.866025403784439,1.,0.866025403784439,1.,0.866025403784439,
1.,0.866025403784439,1.,0.866025403784439,1.,0.866025403784439,1.,0.866025403784439,
1.,0.866025403784439,1.,0.866025403784439,1.,0.866025403784439,1.,0.866025403784439,
1.)))
REPRESENTATION_ITEM('')
SURFACE()
);
#432=(
BOUNDED_SURFACE()
B_SPLINE_SURFACE(3,2,((#18559,#18560,#18561,#18562,#18563,#18564,#18565,
#18566,#18567,#18568,#18569,#18570,#18571,#18572,#18573,#18574,#18575,#18576,
#18577,#18578,#18579,#18580,#18581,#18582,#18583,#18584,#18585,#18586,#18587,
#18588,#18589,#18590,#18591,#18592,#18593,#18594,#18595,#18596,#18597,#18598,
#18599,#18600,#18601,#18602,#18603,#18604,#18605,#18606,#18607,#18608,#18609,
#18610,#18611,#18612,#18613,#18614,#18615,#18616,#18617,#18618,#18619,#18620,
#18621,#18622,#18623,#18624,#18625,#18626,#18627,#18628,#18629,#18630,#18631),
(#18632,#18633,#18634,#18635,#18636,#18637,#18638,#18639,#18640,#18641,
#18642,#18643,#18644,#18645,#18646,#18647,#18648,#18649,#18650,#18651,#18652,
#18653,#18654,#18655,#18656,#18657,#18658,#18659,#18660,#18661,#18662,#18663,
#18664,#18665,#18666,#18667,#18668,#18669,#18670,#18671,#18672,#18673,#18674,
#18675,#18676,#18677,#18678,#18679,#18680,#18681,#18682,#18683,#18684,#18685,
#18686,#18687,#18688,#18689,#18690,#18691,#18692,#18693,#18694,#18695,#18696,
#18697,#18698,#18699,#18700,#18701,#18702,#18703,#18704),(#18705,#18706,
#18707,#18708,#18709,#18710,#18711,#18712,#18713,#18714,#18715,#18716,#18717,
#18718,#18719,#18720,#18721,#18722,#18723,#18724,#18725,#18726,#18727,#18728,
#18729,#18730,#18731,#18732,#18733,#18734,#18735,#18736,#18737,#18738,#18739,
#18740,#18741,#18742,#18743,#18744,#18745,#18746,#18747,#18748,#18749,#18750,
#18751,#18752,#18753,#18754,#18755,#18756,#18757,#18758,#18759,#18760,#18761,
#18762,#18763,#18764,#18765,#18766,#18767,#18768,#18769,#18770,#18771,#18772,
#18773,#18774,#18775,#18776,#18777),(#18778,#18779,#18780,#18781,#18782,
#18783,#18784,#18785,#18786,#18787,#18788,#18789,#18790,#18791,#18792,#18793,
#18794,#18795,#18796,#18797,#18798,#18799,#18800,#18801,#18802,#18803,#18804,
#18805,#18806,#18807,#18808,#18809,#18810,#18811,#18812,#18813,#18814,#18815,
#18816,#18817,#18818,#18819,#18820,#18821,#18822,#18823,#18824,#18825,#18826,
#18827,#18828,#18829,#18830,#18831,#18832,#18833,#18834,#18835,#18836,#18837,
#18838,#18839,#18840,#18841,#18842,#18843,#18844,#18845,#18846,#18847,#18848,
#18849,#18850)),.UNSPECIFIED.,.F.,.F.,.F.)
B_SPLINE_SURFACE_WITH_KNOTS((4,4),(3,2,2,2,2,2,2,2,2,2,2,2,2,2,2,2,2,2,
2,2,2,2,2,2,2,2,2,2,2,2,2,2,2,2,2,2,3),(0.,1.),(0.,0.0277777777777778,0.0555555555555556,
0.0833333333333333,0.111111111111111,0.138888888888889,0.166666666666667,
0.194444444444444,0.222222222222222,0.25,0.277777777777778,0.305555555555556,
0.333333333333333,0.361111111111111,0.388888888888889,0.416666666666667,
0.444444444444444,0.472222222222222,0.5,0.527777777777778,0.555555555555556,
0.583333333333333,0.611111111111111,0.638888888888889,0.666666666666667,
0.694444444444444,0.722222222222222,0.75,0.777777777777778,0.805555555555556,
0.833333333333333,0.861111111111111,0.888888888888889,0.916666666666667,
0.944444444444444,0.972222222222222,1.),.UNSPECIFIED.)
GEOMETRIC_REPRESENTATION_ITEM()
RATIONAL_B_SPLINE_SURFACE(((1.,0.866025403784439,1.,0.866025403784439,1.,
0.866025403784439,1.,0.866025403784439,1.,0.866025403784439,1.,0.866025403784439,
1.,0.866025403784439,1.,0.866025403784439,1.,0.866025403784439,1.,0.866025403784439,
1.,0.866025403784439,1.,0.866025403784439,1.,0.866025403784439,1.,0.866025403784439,
1.,0.866025403784439,1.,0.866025403784439,1.,0.866025403784439,1.,0.866025403784439,
1.,0.866025403784439,1.,0.866025403784439,1.,0.866025403784439,1.,0.866025403784439,
1.,0.866025403784439,1.,0.866025403784439,1.,0.866025403784439,1.,0.866025403784439,
1.,0.866025403784439,1.,0.866025403784439,1.,0.866025403784439,1.,0.866025403784439,
1.,0.866025403784439,1.,0.866025403784439,1.,0.866025403784439,1.,0.866025403784439,
1.,0.866025403784439,1.,0.866025403784439,1.),(0.804737854124365,0.696923425058676,
0.804737854124365,0.696923425058676,0.804737854124365,0.696923425058676,
0.804737854124365,0.696923425058676,0.804737854124365,0.696923425058676,
0.804737854124365,0.696923425058676,0.804737854124365,0.696923425058676,
0.804737854124365,0.696923425058676,0.804737854124365,0.696923425058676,
0.804737854124365,0.696923425058676,0.804737854124365,0.696923425058676,
0.804737854124365,0.696923425058676,0.804737854124365,0.696923425058676,
0.804737854124365,0.696923425058676,0.804737854124365,0.696923425058676,
0.804737854124365,0.696923425058676,0.804737854124365,0.696923425058676,
0.804737854124365,0.696923425058676,0.804737854124365,0.696923425058676,
0.804737854124365,0.696923425058676,0.804737854124365,0.696923425058676,
0.804737854124365,0.696923425058676,0.804737854124365,0.696923425058676,
0.804737854124365,0.696923425058676,0.804737854124365,0.696923425058676,
0.804737854124365,0.696923425058676,0.804737854124365,0.696923425058676,
0.804737854124365,0.696923425058676,0.804737854124365,0.696923425058676,
0.804737854124365,0.696923425058676,0.804737854124365,0.696923425058676,
0.804737854124365,0.696923425058676,0.804737854124365,0.696923425058676,
0.804737854124365,0.696923425058676,0.804737854124365,0.696923425058676,
0.804737854124365,0.696923425058676,0.804737854124365),(0.804737854124365,
0.696923425058676,0.804737854124365,0.696923425058676,0.804737854124365,
0.696923425058676,0.804737854124365,0.696923425058676,0.804737854124365,
0.696923425058676,0.804737854124365,0.696923425058676,0.804737854124365,
0.696923425058676,0.804737854124365,0.696923425058676,0.804737854124365,
0.696923425058676,0.804737854124365,0.696923425058676,0.804737854124365,
0.696923425058676,0.804737854124365,0.696923425058676,0.804737854124365,
0.696923425058676,0.804737854124365,0.696923425058676,0.804737854124365,
0.696923425058676,0.804737854124365,0.696923425058676,0.804737854124365,
0.696923425058676,0.804737854124365,0.696923425058676,0.804737854124365,
0.696923425058676,0.804737854124365,0.696923425058676,0.804737854124365,
0.696923425058676,0.804737854124365,0.696923425058676,0.804737854124365,
0.696923425058676,0.804737854124365,0.696923425058676,0.804737854124365,
0.696923425058676,0.804737854124365,0.696923425058676,0.804737854124365,
0.696923425058676,0.804737854124365,0.696923425058676,0.804737854124365,
0.696923425058676,0.804737854124365,0.696923425058676,0.804737854124365,
0.696923425058676,0.804737854124365,0.696923425058676,0.804737854124365,
0.696923425058676,0.804737854124365,0.696923425058676,0.804737854124365,
0.696923425058676,0.804737854124365,0.696923425058676,0.804737854124365),
(1.,0.866025403784439,1.,0.866025403784439,1.,0.866025403784439,1.,0.866025403784439,
1.,0.866025403784439,1.,0.866025403784439,1.,0.866025403784439,1.,0.866025403784439,
1.,0.866025403784439,1.,0.866025403784439,1.,0.866025403784439,1.,0.866025403784439,
1.,0.866025403784439,1.,0.866025403784439,1.,0.866025403784439,1.,0.866025403784439,
1.,0.866025403784439,1.,0.866025403784439,1.,0.866025403784439,1.,0.866025403784439,
1.,0.866025403784439,1.,0.866025403784439,1.,0.866025403784439,1.,0.866025403784439,
1.,0.866025403784439,1.,0.866025403784439,1.,0.866025403784439,1.,0.866025403784439,
1.,0.866025403784439,1.,0.866025403784439,1.,0.866025403784439,1.,0.866025403784439,
1.,0.866025403784439,1.,0.866025403784439,1.,0.866025403784439,1.,0.866025403784439,
1.)))
REPRESENTATION_ITEM('')
SURFACE()
);
#433=(
BOUNDED_SURFACE()
B_SPLINE_SURFACE(3,2,((#18928,#18929,#18930,#18931,#18932,#18933,#18934,
#18935,#18936,#18937,#18938,#18939,#18940,#18941,#18942,#18943,#18944,#18945,
#18946,#18947,#18948,#18949,#18950,#18951,#18952,#18953,#18954,#18955,#18956,
#18957,#18958,#18959,#18960,#18961,#18962,#18963,#18964,#18965,#18966,#18967,
#18968,#18969,#18970,#18971,#18972,#18973,#18974,#18975,#18976,#18977,#18978,
#18979,#18980,#18981,#18982,#18983,#18984,#18985,#18986,#18987,#18988,#18989,
#18990,#18991,#18992,#18993,#18994,#18995,#18996,#18997,#18998,#18999,#19000),
(#19001,#19002,#19003,#19004,#19005,#19006,#19007,#19008,#19009,#19010,
#19011,#19012,#19013,#19014,#19015,#19016,#19017,#19018,#19019,#19020,#19021,
#19022,#19023,#19024,#19025,#19026,#19027,#19028,#19029,#19030,#19031,#19032,
#19033,#19034,#19035,#19036,#19037,#19038,#19039,#19040,#19041,#19042,#19043,
#19044,#19045,#19046,#19047,#19048,#19049,#19050,#19051,#19052,#19053,#19054,
#19055,#19056,#19057,#19058,#19059,#19060,#19061,#19062,#19063,#19064,#19065,
#19066,#19067,#19068,#19069,#19070,#19071,#19072,#19073),(#19074,#19075,
#19076,#19077,#19078,#19079,#19080,#19081,#19082,#19083,#19084,#19085,#19086,
#19087,#19088,#19089,#19090,#19091,#19092,#19093,#19094,#19095,#19096,#19097,
#19098,#19099,#19100,#19101,#19102,#19103,#19104,#19105,#19106,#19107,#19108,
#19109,#19110,#19111,#19112,#19113,#19114,#19115,#19116,#19117,#19118,#19119,
#19120,#19121,#19122,#19123,#19124,#19125,#19126,#19127,#19128,#19129,#19130,
#19131,#19132,#19133,#19134,#19135,#19136,#19137,#19138,#19139,#19140,#19141,
#19142,#19143,#19144,#19145,#19146),(#19147,#19148,#19149,#19150,#19151,
#19152,#19153,#19154,#19155,#19156,#19157,#19158,#19159,#19160,#19161,#19162,
#19163,#19164,#19165,#19166,#19167,#19168,#19169,#19170,#19171,#19172,#19173,
#19174,#19175,#19176,#19177,#19178,#19179,#19180,#19181,#19182,#19183,#19184,
#19185,#19186,#19187,#19188,#19189,#19190,#19191,#19192,#19193,#19194,#19195,
#19196,#19197,#19198,#19199,#19200,#19201,#19202,#19203,#19204,#19205,#19206,
#19207,#19208,#19209,#19210,#19211,#19212,#19213,#19214,#19215,#19216,#19217,
#19218,#19219)),.UNSPECIFIED.,.F.,.F.,.F.)
B_SPLINE_SURFACE_WITH_KNOTS((4,4),(3,2,2,2,2,2,2,2,2,2,2,2,2,2,2,2,2,2,
2,2,2,2,2,2,2,2,2,2,2,2,2,2,2,2,2,2,3),(0.,1.),(0.,0.0277777777777778,0.0555555555555556,
0.0833333333333333,0.111111111111111,0.138888888888889,0.166666666666667,
0.194444444444444,0.222222222222222,0.25,0.277777777777778,0.305555555555556,
0.333333333333333,0.361111111111111,0.388888888888889,0.416666666666667,
0.444444444444444,0.472222222222222,0.5,0.527777777777778,0.555555555555556,
0.583333333333333,0.611111111111111,0.638888888888889,0.666666666666667,
0.694444444444444,0.722222222222222,0.75,0.777777777777778,0.805555555555556,
0.833333333333333,0.861111111111111,0.888888888888889,0.916666666666667,
0.944444444444444,0.972222222222222,1.),.UNSPECIFIED.)
GEOMETRIC_REPRESENTATION_ITEM()
RATIONAL_B_SPLINE_SURFACE(((1.,0.866025403784439,1.,0.866025403784439,1.,
0.866025403784439,1.,0.866025403784439,1.,0.866025403784439,1.,0.866025403784439,
1.,0.866025403784439,1.,0.866025403784439,1.,0.866025403784439,1.,0.866025403784439,
1.,0.866025403784439,1.,0.866025403784439,1.,0.866025403784439,1.,0.866025403784439,
1.,0.866025403784439,1.,0.866025403784439,1.,0.866025403784439,1.,0.866025403784439,
1.,0.866025403784439,1.,0.866025403784439,1.,0.866025403784439,1.,0.866025403784439,
1.,0.866025403784439,1.,0.866025403784439,1.,0.866025403784439,1.,0.866025403784439,
1.,0.866025403784439,1.,0.866025403784439,1.,0.866025403784439,1.,0.866025403784439,
1.,0.866025403784439,1.,0.866025403784439,1.,0.866025403784439,1.,0.866025403784439,
1.,0.866025403784439,1.,0.866025403784439,1.),(0.804737854124365,0.696923425058676,
0.804737854124365,0.696923425058676,0.804737854124365,0.696923425058676,
0.804737854124365,0.696923425058676,0.804737854124365,0.696923425058676,
0.804737854124365,0.696923425058676,0.804737854124365,0.696923425058676,
0.804737854124365,0.696923425058676,0.804737854124365,0.696923425058676,
0.804737854124365,0.696923425058676,0.804737854124365,0.696923425058676,
0.804737854124365,0.696923425058676,0.804737854124365,0.696923425058676,
0.804737854124365,0.696923425058676,0.804737854124365,0.696923425058676,
0.804737854124365,0.696923425058676,0.804737854124365,0.696923425058676,
0.804737854124365,0.696923425058676,0.804737854124365,0.696923425058676,
0.804737854124365,0.696923425058676,0.804737854124365,0.696923425058676,
0.804737854124365,0.696923425058676,0.804737854124365,0.696923425058676,
0.804737854124365,0.696923425058676,0.804737854124365,0.696923425058676,
0.804737854124365,0.696923425058676,0.804737854124365,0.696923425058676,
0.804737854124365,0.696923425058676,0.804737854124365,0.696923425058676,
0.804737854124365,0.696923425058676,0.804737854124365,0.696923425058676,
0.804737854124365,0.696923425058676,0.804737854124365,0.696923425058676,
0.804737854124365,0.696923425058676,0.804737854124365,0.696923425058676,
0.804737854124365,0.696923425058676,0.804737854124365),(0.804737854124365,
0.696923425058676,0.804737854124365,0.696923425058676,0.804737854124365,
0.696923425058676,0.804737854124365,0.696923425058676,0.804737854124365,
0.696923425058676,0.804737854124365,0.696923425058676,0.804737854124365,
0.696923425058676,0.804737854124365,0.696923425058676,0.804737854124365,
0.696923425058676,0.804737854124365,0.696923425058676,0.804737854124365,
0.696923425058676,0.804737854124365,0.696923425058676,0.804737854124365,
0.696923425058676,0.804737854124365,0.696923425058676,0.804737854124365,
0.696923425058676,0.804737854124365,0.696923425058676,0.804737854124365,
0.696923425058676,0.804737854124365,0.696923425058676,0.804737854124365,
0.696923425058676,0.804737854124365,0.696923425058676,0.804737854124365,
0.696923425058676,0.804737854124365,0.696923425058676,0.804737854124365,
0.696923425058676,0.804737854124365,0.696923425058676,0.804737854124365,
0.696923425058676,0.804737854124365,0.696923425058676,0.804737854124365,
0.696923425058676,0.804737854124365,0.696923425058676,0.804737854124365,
0.696923425058676,0.804737854124365,0.696923425058676,0.804737854124365,
0.696923425058676,0.804737854124365,0.696923425058676,0.804737854124365,
0.696923425058676,0.804737854124365,0.696923425058676,0.804737854124365,
0.696923425058676,0.804737854124365,0.696923425058676,0.804737854124365),
(1.,0.866025403784439,1.,0.866025403784439,1.,0.866025403784439,1.,0.866025403784439,
1.,0.866025403784439,1.,0.866025403784439,1.,0.866025403784439,1.,0.866025403784439,
1.,0.866025403784439,1.,0.866025403784439,1.,0.866025403784439,1.,0.866025403784439,
1.,0.866025403784439,1.,0.866025403784439,1.,0.866025403784439,1.,0.866025403784439,
1.,0.866025403784439,1.,0.866025403784439,1.,0.866025403784439,1.,0.866025403784439,
1.,0.866025403784439,1.,0.866025403784439,1.,0.866025403784439,1.,0.866025403784439,
1.,0.866025403784439,1.,0.866025403784439,1.,0.866025403784439,1.,0.866025403784439,
1.,0.866025403784439,1.,0.866025403784439,1.,0.866025403784439,1.,0.866025403784439,
1.,0.866025403784439,1.,0.866025403784439,1.,0.866025403784439,1.,0.866025403784439,
1.)))
REPRESENTATION_ITEM('')
SURFACE()
);
#434=(
BOUNDED_SURFACE()
B_SPLINE_SURFACE(3,2,((#19297,#19298,#19299,#19300,#19301,#19302,#19303,
#19304,#19305,#19306,#19307,#19308,#19309,#19310,#19311,#19312,#19313,#19314,
#19315,#19316,#19317,#19318,#19319,#19320,#19321,#19322,#19323,#19324,#19325,
#19326,#19327,#19328,#19329,#19330,#19331,#19332,#19333,#19334,#19335,#19336,
#19337,#19338,#19339,#19340,#19341,#19342,#19343,#19344,#19345,#19346,#19347,
#19348,#19349,#19350,#19351,#19352,#19353,#19354,#19355,#19356,#19357,#19358,
#19359,#19360,#19361,#19362,#19363,#19364,#19365,#19366,#19367,#19368,#19369),
(#19370,#19371,#19372,#19373,#19374,#19375,#19376,#19377,#19378,#19379,
#19380,#19381,#19382,#19383,#19384,#19385,#19386,#19387,#19388,#19389,#19390,
#19391,#19392,#19393,#19394,#19395,#19396,#19397,#19398,#19399,#19400,#19401,
#19402,#19403,#19404,#19405,#19406,#19407,#19408,#19409,#19410,#19411,#19412,
#19413,#19414,#19415,#19416,#19417,#19418,#19419,#19420,#19421,#19422,#19423,
#19424,#19425,#19426,#19427,#19428,#19429,#19430,#19431,#19432,#19433,#19434,
#19435,#19436,#19437,#19438,#19439,#19440,#19441,#19442),(#19443,#19444,
#19445,#19446,#19447,#19448,#19449,#19450,#19451,#19452,#19453,#19454,#19455,
#19456,#19457,#19458,#19459,#19460,#19461,#19462,#19463,#19464,#19465,#19466,
#19467,#19468,#19469,#19470,#19471,#19472,#19473,#19474,#19475,#19476,#19477,
#19478,#19479,#19480,#19481,#19482,#19483,#19484,#19485,#19486,#19487,#19488,
#19489,#19490,#19491,#19492,#19493,#19494,#19495,#19496,#19497,#19498,#19499,
#19500,#19501,#19502,#19503,#19504,#19505,#19506,#19507,#19508,#19509,#19510,
#19511,#19512,#19513,#19514,#19515),(#19516,#19517,#19518,#19519,#19520,
#19521,#19522,#19523,#19524,#19525,#19526,#19527,#19528,#19529,#19530,#19531,
#19532,#19533,#19534,#19535,#19536,#19537,#19538,#19539,#19540,#19541,#19542,
#19543,#19544,#19545,#19546,#19547,#19548,#19549,#19550,#19551,#19552,#19553,
#19554,#19555,#19556,#19557,#19558,#19559,#19560,#19561,#19562,#19563,#19564,
#19565,#19566,#19567,#19568,#19569,#19570,#19571,#19572,#19573,#19574,#19575,
#19576,#19577,#19578,#19579,#19580,#19581,#19582,#19583,#19584,#19585,#19586,
#19587,#19588)),.UNSPECIFIED.,.F.,.F.,.F.)
B_SPLINE_SURFACE_WITH_KNOTS((4,4),(3,2,2,2,2,2,2,2,2,2,2,2,2,2,2,2,2,2,
2,2,2,2,2,2,2,2,2,2,2,2,2,2,2,2,2,2,3),(0.,1.),(0.,0.0277777777777778,0.0555555555555556,
0.0833333333333333,0.111111111111111,0.138888888888889,0.166666666666667,
0.194444444444444,0.222222222222222,0.25,0.277777777777778,0.305555555555556,
0.333333333333333,0.361111111111111,0.388888888888889,0.416666666666667,
0.444444444444444,0.472222222222222,0.5,0.527777777777778,0.555555555555556,
0.583333333333333,0.611111111111111,0.638888888888889,0.666666666666667,
0.694444444444444,0.722222222222222,0.75,0.777777777777778,0.805555555555556,
0.833333333333333,0.861111111111111,0.888888888888889,0.916666666666667,
0.944444444444444,0.972222222222222,1.),.UNSPECIFIED.)
GEOMETRIC_REPRESENTATION_ITEM()
RATIONAL_B_SPLINE_SURFACE(((1.,0.866025403784439,1.,0.866025403784439,1.,
0.866025403784439,1.,0.866025403784439,1.,0.866025403784439,1.,0.866025403784439,
1.,0.866025403784439,1.,0.866025403784439,1.,0.866025403784439,1.,0.866025403784439,
1.,0.866025403784439,1.,0.866025403784439,1.,0.866025403784439,1.,0.866025403784439,
1.,0.866025403784439,1.,0.866025403784439,1.,0.866025403784439,1.,0.866025403784439,
1.,0.866025403784439,1.,0.866025403784439,1.,0.866025403784439,1.,0.866025403784439,
1.,0.866025403784439,1.,0.866025403784439,1.,0.866025403784439,1.,0.866025403784439,
1.,0.866025403784439,1.,0.866025403784439,1.,0.866025403784439,1.,0.866025403784439,
1.,0.866025403784439,1.,0.866025403784439,1.,0.866025403784439,1.,0.866025403784439,
1.,0.866025403784439,1.,0.866025403784439,1.),(0.804737854124365,0.696923425058676,
0.804737854124365,0.696923425058676,0.804737854124365,0.696923425058676,
0.804737854124365,0.696923425058676,0.804737854124365,0.696923425058676,
0.804737854124365,0.696923425058676,0.804737854124365,0.696923425058676,
0.804737854124365,0.696923425058676,0.804737854124365,0.696923425058676,
0.804737854124365,0.696923425058676,0.804737854124365,0.696923425058676,
0.804737854124365,0.696923425058676,0.804737854124365,0.696923425058676,
0.804737854124365,0.696923425058676,0.804737854124365,0.696923425058676,
0.804737854124365,0.696923425058676,0.804737854124365,0.696923425058676,
0.804737854124365,0.696923425058676,0.804737854124365,0.696923425058676,
0.804737854124365,0.696923425058676,0.804737854124365,0.696923425058676,
0.804737854124365,0.696923425058676,0.804737854124365,0.696923425058676,
0.804737854124365,0.696923425058676,0.804737854124365,0.696923425058676,
0.804737854124365,0.696923425058676,0.804737854124365,0.696923425058676,
0.804737854124365,0.696923425058676,0.804737854124365,0.696923425058676,
0.804737854124365,0.696923425058676,0.804737854124365,0.696923425058676,
0.804737854124365,0.696923425058676,0.804737854124365,0.696923425058676,
0.804737854124365,0.696923425058676,0.804737854124365,0.696923425058676,
0.804737854124365,0.696923425058676,0.804737854124365),(0.804737854124365,
0.696923425058676,0.804737854124365,0.696923425058676,0.804737854124365,
0.696923425058676,0.804737854124365,0.696923425058676,0.804737854124365,
0.696923425058676,0.804737854124365,0.696923425058676,0.804737854124365,
0.696923425058676,0.804737854124365,0.696923425058676,0.804737854124365,
0.696923425058676,0.804737854124365,0.696923425058676,0.804737854124365,
0.696923425058676,0.804737854124365,0.696923425058676,0.804737854124365,
0.696923425058676,0.804737854124365,0.696923425058676,0.804737854124365,
0.696923425058676,0.804737854124365,0.696923425058676,0.804737854124365,
0.696923425058676,0.804737854124365,0.696923425058676,0.804737854124365,
0.696923425058676,0.804737854124365,0.696923425058676,0.804737854124365,
0.696923425058676,0.804737854124365,0.696923425058676,0.804737854124365,
0.696923425058676,0.804737854124365,0.696923425058676,0.804737854124365,
0.696923425058676,0.804737854124365,0.696923425058676,0.804737854124365,
0.696923425058676,0.804737854124365,0.696923425058676,0.804737854124365,
0.696923425058676,0.804737854124365,0.696923425058676,0.804737854124365,
0.696923425058676,0.804737854124365,0.696923425058676,0.804737854124365,
0.696923425058676,0.804737854124365,0.696923425058676,0.804737854124365,
0.696923425058676,0.804737854124365,0.696923425058676,0.804737854124365),
(1.,0.866025403784439,1.,0.866025403784439,1.,0.866025403784439,1.,0.866025403784439,
1.,0.866025403784439,1.,0.866025403784439,1.,0.866025403784439,1.,0.866025403784439,
1.,0.866025403784439,1.,0.866025403784439,1.,0.866025403784439,1.,0.866025403784439,
1.,0.866025403784439,1.,0.866025403784439,1.,0.866025403784439,1.,0.866025403784439,
1.,0.866025403784439,1.,0.866025403784439,1.,0.866025403784439,1.,0.866025403784439,
1.,0.866025403784439,1.,0.866025403784439,1.,0.866025403784439,1.,0.866025403784439,
1.,0.866025403784439,1.,0.866025403784439,1.,0.866025403784439,1.,0.866025403784439,
1.,0.866025403784439,1.,0.866025403784439,1.,0.866025403784439,1.,0.866025403784439,
1.,0.866025403784439,1.,0.866025403784439,1.,0.866025403784439,1.,0.866025403784439,
1.)))
REPRESENTATION_ITEM('')
SURFACE()
);
#894=PLANE('',#10675);
#895=PLANE('',#10676);
#1256=FACE_OUTER_BOUND('',#1834,.T.);
#1257=FACE_OUTER_BOUND('',#1835,.T.);
#1258=FACE_OUTER_BOUND('',#1836,.T.);
#1259=FACE_OUTER_BOUND('',#1837,.T.);
#1260=FACE_OUTER_BOUND('',#1838,.T.);
#1261=FACE_OUTER_BOUND('',#1839,.T.);
#1834=EDGE_LOOP('',(#7666,#7667,#7668,#7669,#7670));
#1835=EDGE_LOOP('',(#7671,#7672,#7673,#7674,#7675));
#1836=EDGE_LOOP('',(#7676,#7677,#7678,#7679,#7680));
#1837=EDGE_LOOP('',(#7681,#7682,#7683,#7684,#7685));
#1838=EDGE_LOOP('',(#7686,#7687,#7688,#7689));
#1839=EDGE_LOOP('',(#7690,#7691,#7692,#7693));
#2379=CIRCLE('',#10667,0.35);
#2380=CIRCLE('',#10668,0.35);
#2381=CIRCLE('',#10669,0.35);
#2382=CIRCLE('',#10670,0.35);
#2383=CIRCLE('',#10671,0.35);
#2384=CIRCLE('',#10672,0.35);
#2385=CIRCLE('',#10673,0.35);
#2386=CIRCLE('',#10674,0.35);
#4507=VERTEX_POINT('',#18405);
#4508=VERTEX_POINT('',#18406);
#4509=VERTEX_POINT('',#18408);
#4510=VERTEX_POINT('',#18422);
#4511=VERTEX_POINT('',#18484);
#4512=VERTEX_POINT('',#18851);
#4513=VERTEX_POINT('',#19220);
#4514=VERTEX_POINT('',#19222);
#5646=EDGE_CURVE('',#4507,#4508,#2379,.T.);
#5647=EDGE_CURVE('',#4509,#4508,#190,.T.);
#5648=EDGE_CURVE('',#4510,#4509,#191,.T.);
#5649=EDGE_CURVE('',#4511,#4510,#2380,.T.);
#5650=EDGE_CURVE('',#4511,#4507,#192,.T.);
#5651=EDGE_CURVE('',#4512,#4511,#2381,.T.);
#5652=EDGE_CURVE('',#4512,#4510,#193,.T.);
#5653=EDGE_CURVE('',#4510,#4509,#194,.T.);
#5654=EDGE_CURVE('',#4509,#4507,#2382,.T.);
#5655=EDGE_CURVE('',#4513,#4512,#2383,.T.);
#5656=EDGE_CURVE('',#4513,#4514,#195,.T.);
#5657=EDGE_CURVE('',#4514,#4509,#2384,.T.);
#5658=EDGE_CURVE('',#4510,#4513,#2385,.T.);
#5659=EDGE_CURVE('',#4508,#4514,#2386,.T.);
#7666=ORIENTED_EDGE('',*,*,#5646,.T.);
#7667=ORIENTED_EDGE('',*,*,#5647,.F.);
#7668=ORIENTED_EDGE('',*,*,#5648,.F.);
#7669=ORIENTED_EDGE('',*,*,#5649,.F.);
#7670=ORIENTED_EDGE('',*,*,#5650,.T.);
#7671=ORIENTED_EDGE('',*,*,#5650,.F.);
#7672=ORIENTED_EDGE('',*,*,#5651,.F.);
#7673=ORIENTED_EDGE('',*,*,#5652,.T.);
#7674=ORIENTED_EDGE('',*,*,#5653,.T.);
#7675=ORIENTED_EDGE('',*,*,#5654,.T.);
#7676=ORIENTED_EDGE('',*,*,#5652,.F.);
#7677=ORIENTED_EDGE('',*,*,#5655,.F.);
#7678=ORIENTED_EDGE('',*,*,#5656,.T.);
#7679=ORIENTED_EDGE('',*,*,#5657,.T.);
#7680=ORIENTED_EDGE('',*,*,#5653,.F.);
#7681=ORIENTED_EDGE('',*,*,#5656,.F.);
#7682=ORIENTED_EDGE('',*,*,#5658,.F.);
#7683=ORIENTED_EDGE('',*,*,#5648,.T.);
#7684=ORIENTED_EDGE('',*,*,#5647,.T.);
#7685=ORIENTED_EDGE('',*,*,#5659,.T.);
#7686=ORIENTED_EDGE('',*,*,#5659,.F.);
#7687=ORIENTED_EDGE('',*,*,#5646,.F.);
#7688=ORIENTED_EDGE('',*,*,#5654,.F.);
#7689=ORIENTED_EDGE('',*,*,#5657,.F.);
#7690=ORIENTED_EDGE('',*,*,#5658,.T.);
#7691=ORIENTED_EDGE('',*,*,#5655,.T.);
#7692=ORIENTED_EDGE('',*,*,#5651,.T.);
#7693=ORIENTED_EDGE('',*,*,#5649,.T.);
#9622=ADVANCED_FACE('',(#1256),#431,.F.);
#9623=ADVANCED_FACE('',(#1257),#432,.F.);
#9624=ADVANCED_FACE('',(#1258),#433,.F.);
#9625=ADVANCED_FACE('',(#1259),#434,.F.);
#9626=ADVANCED_FACE('',(#1260),#894,.F.);
#9627=ADVANCED_FACE('',(#1261),#895,.T.);
#9947=CLOSED_SHELL('',(#9622,#9623,#9624,#9625,#9626,#9627));
#10666=AXIS2_PLACEMENT_3D('',#18112,#12445,#12446);
#10667=AXIS2_PLACEMENT_3D('',#18407,#12447,#12448);
#10668=AXIS2_PLACEMENT_3D('',#18485,#12449,#12450);
#10669=AXIS2_PLACEMENT_3D('',#18852,#12451,#12452);
#10670=AXIS2_PLACEMENT_3D('',#18927,#12453,#12454);
#10671=AXIS2_PLACEMENT_3D('',#19221,#12455,#12456);
#10672=AXIS2_PLACEMENT_3D('',#19296,#12457,#12458);
#10673=AXIS2_PLACEMENT_3D('',#19589,#12459,#12460);
#10674=AXIS2_PLACEMENT_3D('',#19590,#12461,#12462);
#10675=AXIS2_PLACEMENT_3D('',#19591,#12463,#12464);
#10676=AXIS2_PLACEMENT_3D('',#19592,#12465,#12466);
#12445=DIRECTION('axis',(0.,0.,1.));
#12446=DIRECTION('refdir',(1.,0.,0.));
#12447=DIRECTION('center_axis',(1.,0.,8.37955521322352E-14));
#12448=DIRECTION('ref_axis',(8.37955521322352E-14,0.,-1.));
#12449=DIRECTION('center_axis',(1.,0.,0.));
#12450=DIRECTION('ref_axis',(0.,0.,-1.));
#12451=DIRECTION('center_axis',(1.,0.,0.));
#12452=DIRECTION('ref_axis',(0.,0.,-1.));
#12453=DIRECTION('center_axis',(1.,0.,8.37955521322352E-14));
#12454=DIRECTION('ref_axis',(8.37955521322352E-14,0.,-1.));
#12455=DIRECTION('center_axis',(1.,0.,0.));
#12456=DIRECTION('ref_axis',(0.,0.,-1.));
#12457=DIRECTION('center_axis',(1.,0.,8.37955521322352E-14));
#12458=DIRECTION('ref_axis',(8.37955521322352E-14,0.,-1.));
#12459=DIRECTION('center_axis',(1.,0.,0.));
#12460=DIRECTION('ref_axis',(0.,0.,-1.));
#12461=DIRECTION('center_axis',(1.,0.,8.37955521322352E-14));
#12462=DIRECTION('ref_axis',(8.37955521322352E-14,0.,-1.));
#12463=DIRECTION('center_axis',(1.,0.,8.37955521322352E-14));
#12464=DIRECTION('ref_axis',(8.37955521322352E-14,0.,-1.));
#12465=DIRECTION('center_axis',(1.,0.,0.));
#12466=DIRECTION('ref_axis',(0.,0.,-1.));
#18112=CARTESIAN_POINT('',(0.,0.,0.));
#18113=CARTESIAN_POINT('Ctrl Pts',(0.,0.,1.8));
#18114=CARTESIAN_POINT('Ctrl Pts',(-1.03923048454133,0.0583333333333332,
1.8));
#18115=CARTESIAN_POINT('Ctrl Pts',(-1.55884572681199,0.116666666666666,
0.9));
#18116=CARTESIAN_POINT('Ctrl Pts',(-2.07846096908265,0.175,1.27269028646989E-16));
#18117=CARTESIAN_POINT('Ctrl Pts',(-1.55884572681199,0.233333333333333,
-0.9));
#18118=CARTESIAN_POINT('Ctrl Pts',(-1.03923048454133,0.291666666666666,
-1.8));
#18119=CARTESIAN_POINT('Ctrl Pts',(-2.20436423846524E-16,0.349999999999999,
-1.8));
#18120=CARTESIAN_POINT('Ctrl Pts',(1.03923048454133,0.408333333333333,-1.8));
#18121=CARTESIAN_POINT('Ctrl Pts',(1.55884572681199,0.466666666666666,-0.900000000000001));
#18122=CARTESIAN_POINT('Ctrl Pts',(2.07846096908265,0.524999999999999,-3.81807085940967E-16));
#18123=CARTESIAN_POINT('Ctrl Pts',(1.55884572681199,0.583333333333332,0.899999999999999));
#18124=CARTESIAN_POINT('Ctrl Pts',(1.03923048454133,0.641666666666665,1.8));
#18125=CARTESIAN_POINT('Ctrl Pts',(0.,0.699999999999999,1.8));
#18126=CARTESIAN_POINT('Ctrl Pts',(-1.03923048454133,0.758333333333332,
1.8));
#18127=CARTESIAN_POINT('Ctrl Pts',(-1.55884572681199,0.816666666666665,
0.9));
#18128=CARTESIAN_POINT('Ctrl Pts',(-2.07846096908265,0.874999999999998,
1.27269028646989E-16));
#18129=CARTESIAN_POINT('Ctrl Pts',(-1.55884572681199,0.933333333333332,
-0.9));
#18130=CARTESIAN_POINT('Ctrl Pts',(-1.03923048454133,0.991666666666665,
-1.8));
#18131=CARTESIAN_POINT('Ctrl Pts',(-2.20436423846524E-16,1.05,-1.8));
#18132=CARTESIAN_POINT('Ctrl Pts',(1.03923048454133,1.10833333333333,-1.8));
#18133=CARTESIAN_POINT('Ctrl Pts',(1.55884572681199,1.16666666666666,-0.900000000000001));
#18134=CARTESIAN_POINT('Ctrl Pts',(2.07846096908265,1.225,-3.81807085940967E-16));
#18135=CARTESIAN_POINT('Ctrl Pts',(1.55884572681199,1.28333333333333,0.899999999999999));
#18136=CARTESIAN_POINT('Ctrl Pts',(1.03923048454133,1.34166666666666,1.8));
#18137=CARTESIAN_POINT('Ctrl Pts',(0.,1.4,1.8));
#18138=CARTESIAN_POINT('Ctrl Pts',(-1.03923048454133,1.45833333333333,1.8));
#18139=CARTESIAN_POINT('Ctrl Pts',(-1.55884572681199,1.51666666666666,0.9));
#18140=CARTESIAN_POINT('Ctrl Pts',(-2.07846096908265,1.575,1.27269028646989E-16));
#18141=CARTESIAN_POINT('Ctrl Pts',(-1.55884572681199,1.63333333333333,-0.9));
#18142=CARTESIAN_POINT('Ctrl Pts',(-1.03923048454133,1.69166666666666,-1.8));
#18143=CARTESIAN_POINT('Ctrl Pts',(-2.20436423846524E-16,1.75,-1.8));
#18144=CARTESIAN_POINT('Ctrl Pts',(1.03923048454133,1.80833333333333,-1.8));
#18145=CARTESIAN_POINT('Ctrl Pts',(1.55884572681199,1.86666666666666,-0.900000000000001));
#18146=CARTESIAN_POINT('Ctrl Pts',(2.07846096908265,1.925,-3.81807085940967E-16));
#18147=CARTESIAN_POINT('Ctrl Pts',(1.55884572681199,1.98333333333333,0.899999999999999));
#18148=CARTESIAN_POINT('Ctrl Pts',(1.03923048454133,2.04166666666666,1.8));
#18149=CARTESIAN_POINT('Ctrl Pts',(0.,2.1,1.8));
#18150=CARTESIAN_POINT('Ctrl Pts',(-1.03923048454133,2.15833333333333,1.8));
#18151=CARTESIAN_POINT('Ctrl Pts',(-1.55884572681199,2.21666666666666,0.9));
#18152=CARTESIAN_POINT('Ctrl Pts',(-2.07846096908265,2.275,1.27269028646989E-16));
#18153=CARTESIAN_POINT('Ctrl Pts',(-1.55884572681199,2.33333333333333,-0.9));
#18154=CARTESIAN_POINT('Ctrl Pts',(-1.03923048454133,2.39166666666666,-1.8));
#18155=CARTESIAN_POINT('Ctrl Pts',(-2.20436423846524E-16,2.45,-1.8));
#18156=CARTESIAN_POINT('Ctrl Pts',(1.03923048454133,2.50833333333333,-1.8));
#18157=CARTESIAN_POINT('Ctrl Pts',(1.55884572681199,2.56666666666666,-0.900000000000001));
#18158=CARTESIAN_POINT('Ctrl Pts',(2.07846096908265,2.62499999999999,-3.81807085940967E-16));
#18159=CARTESIAN_POINT('Ctrl Pts',(1.55884572681199,2.68333333333333,0.899999999999999));
#18160=CARTESIAN_POINT('Ctrl Pts',(1.03923048454133,2.74166666666666,1.8));
#18161=CARTESIAN_POINT('Ctrl Pts',(0.,2.79999999999999,1.8));
#18162=CARTESIAN_POINT('Ctrl Pts',(-1.03923048454133,2.85833333333333,1.8));
#18163=CARTESIAN_POINT('Ctrl Pts',(-1.55884572681199,2.91666666666666,0.9));
#18164=CARTESIAN_POINT('Ctrl Pts',(-2.07846096908265,2.97499999999999,1.27269028646989E-16));
#18165=CARTESIAN_POINT('Ctrl Pts',(-1.55884572681199,3.03333333333333,-0.9));
#18166=CARTESIAN_POINT('Ctrl Pts',(-1.03923048454133,3.09166666666666,-1.8));
#18167=CARTESIAN_POINT('Ctrl Pts',(-2.20436423846524E-16,3.14999999999999,
-1.8));
#18168=CARTESIAN_POINT('Ctrl Pts',(1.03923048454133,3.20833333333333,-1.8));
#18169=CARTESIAN_POINT('Ctrl Pts',(1.55884572681199,3.26666666666666,-0.900000000000001));
#18170=CARTESIAN_POINT('Ctrl Pts',(2.07846096908265,3.32499999999999,-3.81807085940967E-16));
#18171=CARTESIAN_POINT('Ctrl Pts',(1.55884572681199,3.38333333333333,0.899999999999999));
#18172=CARTESIAN_POINT('Ctrl Pts',(1.03923048454133,3.44166666666666,1.8));
#18173=CARTESIAN_POINT('Ctrl Pts',(0.,3.49999999999999,1.8));
#18174=CARTESIAN_POINT('Ctrl Pts',(-1.03923048454133,3.55833333333333,1.8));
#18175=CARTESIAN_POINT('Ctrl Pts',(-1.55884572681199,3.61666666666666,0.9));
#18176=CARTESIAN_POINT('Ctrl Pts',(-2.07846096908265,3.67499999999999,1.27269028646989E-16));
#18177=CARTESIAN_POINT('Ctrl Pts',(-1.55884572681199,3.73333333333333,-0.9));
#18178=CARTESIAN_POINT('Ctrl Pts',(-1.03923048454133,3.79166666666666,-1.8));
#18179=CARTESIAN_POINT('Ctrl Pts',(-2.20436423846524E-16,3.84999999999999,
-1.8));
#18180=CARTESIAN_POINT('Ctrl Pts',(1.03923048454133,3.90833333333333,-1.8));
#18181=CARTESIAN_POINT('Ctrl Pts',(1.55884572681199,3.96666666666666,-0.900000000000001));
#18182=CARTESIAN_POINT('Ctrl Pts',(2.07846096908265,4.02499999999999,-3.81807085940967E-16));
#18183=CARTESIAN_POINT('Ctrl Pts',(1.55884572681199,4.08333333333333,0.899999999999999));
#18184=CARTESIAN_POINT('Ctrl Pts',(1.03923048454133,4.14166666666666,1.8));
#18185=CARTESIAN_POINT('Ctrl Pts',(0.,4.19999999999999,1.8));
#18186=CARTESIAN_POINT('Ctrl Pts',(0.,0.205025253169417,1.8));
#18187=CARTESIAN_POINT('Ctrl Pts',(-1.03923048454133,0.26335858650275,1.8));
#18188=CARTESIAN_POINT('Ctrl Pts',(-1.55884572681199,0.321691919836083,
0.9));
#18189=CARTESIAN_POINT('Ctrl Pts',(-2.07846096908265,0.380025253169416,
1.27269028646989E-16));
#18190=CARTESIAN_POINT('Ctrl Pts',(-1.55884572681199,0.43835858650275,-0.9));
#18191=CARTESIAN_POINT('Ctrl Pts',(-1.03923048454133,0.496691919836083,
-1.8));
#18192=CARTESIAN_POINT('Ctrl Pts',(-2.20436423846524E-16,0.555025253169416,
-1.8));
#18193=CARTESIAN_POINT('Ctrl Pts',(1.03923048454133,0.613358586502749,-1.8));
#18194=CARTESIAN_POINT('Ctrl Pts',(1.55884572681199,0.671691919836083,-0.900000000000001));
#18195=CARTESIAN_POINT('Ctrl Pts',(2.07846096908265,0.730025253169416,-3.81807085940967E-16));
#18196=CARTESIAN_POINT('Ctrl Pts',(1.55884572681199,0.788358586502749,0.899999999999999));
#18197=CARTESIAN_POINT('Ctrl Pts',(1.03923048454133,0.846691919836082,1.8));
#18198=CARTESIAN_POINT('Ctrl Pts',(0.,0.905025253169415,1.8));
#18199=CARTESIAN_POINT('Ctrl Pts',(-1.03923048454133,0.963358586502749,
1.8));
#18200=CARTESIAN_POINT('Ctrl Pts',(-1.55884572681199,1.02169191983608,0.9));
#18201=CARTESIAN_POINT('Ctrl Pts',(-2.07846096908265,1.08002525316942,1.27269028646989E-16));
#18202=CARTESIAN_POINT('Ctrl Pts',(-1.55884572681199,1.13835858650275,-0.9));
#18203=CARTESIAN_POINT('Ctrl Pts',(-1.03923048454133,1.19669191983608,-1.8));
#18204=CARTESIAN_POINT('Ctrl Pts',(-2.20436423846524E-16,1.25502525316941,
-1.8));
#18205=CARTESIAN_POINT('Ctrl Pts',(1.03923048454133,1.31335858650275,-1.8));
#18206=CARTESIAN_POINT('Ctrl Pts',(1.55884572681199,1.37169191983608,-0.900000000000001));
#18207=CARTESIAN_POINT('Ctrl Pts',(2.07846096908265,1.43002525316941,-3.81807085940967E-16));
#18208=CARTESIAN_POINT('Ctrl Pts',(1.55884572681199,1.48835858650275,0.899999999999999));
#18209=CARTESIAN_POINT('Ctrl Pts',(1.03923048454133,1.54669191983608,1.8));
#18210=CARTESIAN_POINT('Ctrl Pts',(0.,1.60502525316941,1.8));
#18211=CARTESIAN_POINT('Ctrl Pts',(-1.03923048454133,1.66335858650275,1.8));
#18212=CARTESIAN_POINT('Ctrl Pts',(-1.55884572681199,1.72169191983608,0.9));
#18213=CARTESIAN_POINT('Ctrl Pts',(-2.07846096908265,1.78002525316941,1.27269028646989E-16));
#18214=CARTESIAN_POINT('Ctrl Pts',(-1.55884572681199,1.83835858650275,-0.9));
#18215=CARTESIAN_POINT('Ctrl Pts',(-1.03923048454133,1.89669191983608,-1.8));
#18216=CARTESIAN_POINT('Ctrl Pts',(-2.20436423846524E-16,1.95502525316941,
-1.8));
#18217=CARTESIAN_POINT('Ctrl Pts',(1.03923048454133,2.01335858650275,-1.8));
#18218=CARTESIAN_POINT('Ctrl Pts',(1.55884572681199,2.07169191983608,-0.900000000000001));
#18219=CARTESIAN_POINT('Ctrl Pts',(2.07846096908265,2.13002525316941,-3.81807085940967E-16));
#18220=CARTESIAN_POINT('Ctrl Pts',(1.55884572681199,2.18835858650275,0.899999999999999));
#18221=CARTESIAN_POINT('Ctrl Pts',(1.03923048454133,2.24669191983608,1.8));
#18222=CARTESIAN_POINT('Ctrl Pts',(0.,2.30502525316941,1.8));
#18223=CARTESIAN_POINT('Ctrl Pts',(-1.03923048454133,2.36335858650275,1.8));
#18224=CARTESIAN_POINT('Ctrl Pts',(-1.55884572681199,2.42169191983608,0.9));
#18225=CARTESIAN_POINT('Ctrl Pts',(-2.07846096908265,2.48002525316941,1.27269028646989E-16));
#18226=CARTESIAN_POINT('Ctrl Pts',(-1.55884572681199,2.53835858650275,-0.9));
#18227=CARTESIAN_POINT('Ctrl Pts',(-1.03923048454133,2.59669191983608,-1.8));
#18228=CARTESIAN_POINT('Ctrl Pts',(-2.20436423846524E-16,2.65502525316941,
-1.8));
#18229=CARTESIAN_POINT('Ctrl Pts',(1.03923048454133,2.71335858650274,-1.8));
#18230=CARTESIAN_POINT('Ctrl Pts',(1.55884572681199,2.77169191983608,-0.900000000000001));
#18231=CARTESIAN_POINT('Ctrl Pts',(2.07846096908265,2.83002525316941,-3.81807085940967E-16));
#18232=CARTESIAN_POINT('Ctrl Pts',(1.55884572681199,2.88835858650274,0.899999999999999));
#18233=CARTESIAN_POINT('Ctrl Pts',(1.03923048454133,2.94669191983608,1.8));
#18234=CARTESIAN_POINT('Ctrl Pts',(0.,3.00502525316941,1.8));
#18235=CARTESIAN_POINT('Ctrl Pts',(-1.03923048454133,3.06335858650274,1.8));
#18236=CARTESIAN_POINT('Ctrl Pts',(-1.55884572681199,3.12169191983608,0.9));
#18237=CARTESIAN_POINT('Ctrl Pts',(-2.07846096908265,3.18002525316941,1.27269028646989E-16));
#18238=CARTESIAN_POINT('Ctrl Pts',(-1.55884572681199,3.23835858650274,-0.9));
#18239=CARTESIAN_POINT('Ctrl Pts',(-1.03923048454133,3.29669191983608,-1.8));
#18240=CARTESIAN_POINT('Ctrl Pts',(-2.20436423846524E-16,3.35502525316941,
-1.8));
#18241=CARTESIAN_POINT('Ctrl Pts',(1.03923048454133,3.41335858650274,-1.8));
#18242=CARTESIAN_POINT('Ctrl Pts',(1.55884572681199,3.47169191983608,-0.900000000000001));
#18243=CARTESIAN_POINT('Ctrl Pts',(2.07846096908265,3.53002525316941,-3.81807085940967E-16));
#18244=CARTESIAN_POINT('Ctrl Pts',(1.55884572681199,3.58835858650274,0.899999999999999));
#18245=CARTESIAN_POINT('Ctrl Pts',(1.03923048454133,3.64669191983608,1.8));
#18246=CARTESIAN_POINT('Ctrl Pts',(0.,3.70502525316941,1.8));
#18247=CARTESIAN_POINT('Ctrl Pts',(-1.03923048454133,3.76335858650274,1.8));
#18248=CARTESIAN_POINT('Ctrl Pts',(-1.55884572681199,3.82169191983608,0.9));
#18249=CARTESIAN_POINT('Ctrl Pts',(-2.07846096908265,3.88002525316941,1.27269028646989E-16));
#18250=CARTESIAN_POINT('Ctrl Pts',(-1.55884572681199,3.93835858650274,-0.9));
#18251=CARTESIAN_POINT('Ctrl Pts',(-1.03923048454133,3.99669191983608,-1.8));
#18252=CARTESIAN_POINT('Ctrl Pts',(-2.20436423846524E-16,4.05502525316941,
-1.8));
#18253=CARTESIAN_POINT('Ctrl Pts',(1.03923048454133,4.11335858650274,-1.8));
#18254=CARTESIAN_POINT('Ctrl Pts',(1.55884572681199,4.17169191983608,-0.900000000000001));
#18255=CARTESIAN_POINT('Ctrl Pts',(2.07846096908265,4.23002525316941,-3.81807085940967E-16));
#18256=CARTESIAN_POINT('Ctrl Pts',(1.55884572681199,4.28835858650274,0.899999999999999));
#18257=CARTESIAN_POINT('Ctrl Pts',(1.03923048454133,4.34669191983608,1.8));
#18258=CARTESIAN_POINT('Ctrl Pts',(0.,4.40502525316941,1.8));
#18259=CARTESIAN_POINT('Ctrl Pts',(0.,0.35,1.94497474683058));
#18260=CARTESIAN_POINT('Ctrl Pts',(-1.12293169364966,0.408333333333333,
1.94497474683058));
#18261=CARTESIAN_POINT('Ctrl Pts',(-1.68439754047449,0.466666666666666,
0.972487373415292));
#18262=CARTESIAN_POINT('Ctrl Pts',(-2.24586338729932,0.525,1.37519470428917E-16));
#18263=CARTESIAN_POINT('Ctrl Pts',(-1.68439754047449,0.583333333333333,
-0.972487373415291));
#18264=CARTESIAN_POINT('Ctrl Pts',(-1.12293169364966,0.641666666666666,
-1.94497474683058));
#18265=CARTESIAN_POINT('Ctrl Pts',(-2.38190709812851E-16,0.699999999999999,
-1.94497474683058));
#18266=CARTESIAN_POINT('Ctrl Pts',(1.12293169364966,0.758333333333333,-1.94497474683058));
#18267=CARTESIAN_POINT('Ctrl Pts',(1.68439754047449,0.816666666666666,-0.972487373415292));
#18268=CARTESIAN_POINT('Ctrl Pts',(2.24586338729932,0.874999999999999,-4.12558411286752E-16));
#18269=CARTESIAN_POINT('Ctrl Pts',(1.68439754047449,0.933333333333332,0.97248737341529));
#18270=CARTESIAN_POINT('Ctrl Pts',(1.12293169364966,0.991666666666665,1.94497474683058));
#18271=CARTESIAN_POINT('Ctrl Pts',(0.,1.05,1.94497474683058));
#18272=CARTESIAN_POINT('Ctrl Pts',(-1.12293169364966,1.10833333333333,1.94497474683058));
#18273=CARTESIAN_POINT('Ctrl Pts',(-1.68439754047449,1.16666666666666,0.972487373415292));
#18274=CARTESIAN_POINT('Ctrl Pts',(-2.24586338729932,1.225,1.37519470428917E-16));
#18275=CARTESIAN_POINT('Ctrl Pts',(-1.68439754047449,1.28333333333333,-0.972487373415291));
#18276=CARTESIAN_POINT('Ctrl Pts',(-1.12293169364966,1.34166666666667,-1.94497474683058));
#18277=CARTESIAN_POINT('Ctrl Pts',(-2.38190709812851E-16,1.4,-1.94497474683058));
#18278=CARTESIAN_POINT('Ctrl Pts',(1.12293169364966,1.45833333333333,-1.94497474683058));
#18279=CARTESIAN_POINT('Ctrl Pts',(1.68439754047449,1.51666666666666,-0.972487373415292));
#18280=CARTESIAN_POINT('Ctrl Pts',(2.24586338729932,1.575,-4.12558411286752E-16));
#18281=CARTESIAN_POINT('Ctrl Pts',(1.68439754047449,1.63333333333333,0.97248737341529));
#18282=CARTESIAN_POINT('Ctrl Pts',(1.12293169364966,1.69166666666666,1.94497474683058));
#18283=CARTESIAN_POINT('Ctrl Pts',(0.,1.75,1.94497474683058));
#18284=CARTESIAN_POINT('Ctrl Pts',(-1.12293169364966,1.80833333333333,1.94497474683058));
#18285=CARTESIAN_POINT('Ctrl Pts',(-1.68439754047449,1.86666666666666,0.972487373415292));
#18286=CARTESIAN_POINT('Ctrl Pts',(-2.24586338729932,1.925,1.37519470428917E-16));
#18287=CARTESIAN_POINT('Ctrl Pts',(-1.68439754047449,1.98333333333333,-0.972487373415291));
#18288=CARTESIAN_POINT('Ctrl Pts',(-1.12293169364966,2.04166666666666,-1.94497474683058));
#18289=CARTESIAN_POINT('Ctrl Pts',(-2.38190709812851E-16,2.1,-1.94497474683058));
#18290=CARTESIAN_POINT('Ctrl Pts',(1.12293169364966,2.15833333333333,-1.94497474683058));
#18291=CARTESIAN_POINT('Ctrl Pts',(1.68439754047449,2.21666666666666,-0.972487373415292));
#18292=CARTESIAN_POINT('Ctrl Pts',(2.24586338729932,2.275,-4.12558411286752E-16));
#18293=CARTESIAN_POINT('Ctrl Pts',(1.68439754047449,2.33333333333333,0.97248737341529));
#18294=CARTESIAN_POINT('Ctrl Pts',(1.12293169364966,2.39166666666666,1.94497474683058));
#18295=CARTESIAN_POINT('Ctrl Pts',(0.,2.45,1.94497474683058));
#18296=CARTESIAN_POINT('Ctrl Pts',(-1.12293169364966,2.50833333333333,1.94497474683058));
#18297=CARTESIAN_POINT('Ctrl Pts',(-1.68439754047449,2.56666666666666,0.972487373415292));
#18298=CARTESIAN_POINT('Ctrl Pts',(-2.24586338729932,2.62499999999999,1.37519470428917E-16));
#18299=CARTESIAN_POINT('Ctrl Pts',(-1.68439754047449,2.68333333333333,-0.972487373415291));
#18300=CARTESIAN_POINT('Ctrl Pts',(-1.12293169364966,2.74166666666666,-1.94497474683058));
#18301=CARTESIAN_POINT('Ctrl Pts',(-2.38190709812851E-16,2.8,-1.94497474683058));
#18302=CARTESIAN_POINT('Ctrl Pts',(1.12293169364966,2.85833333333333,-1.94497474683058));
#18303=CARTESIAN_POINT('Ctrl Pts',(1.68439754047449,2.91666666666666,-0.972487373415292));
#18304=CARTESIAN_POINT('Ctrl Pts',(2.24586338729932,2.97499999999999,-4.12558411286752E-16));
#18305=CARTESIAN_POINT('Ctrl Pts',(1.68439754047449,3.03333333333333,0.97248737341529));
#18306=CARTESIAN_POINT('Ctrl Pts',(1.12293169364966,3.09166666666666,1.94497474683058));
#18307=CARTESIAN_POINT('Ctrl Pts',(0.,3.14999999999999,1.94497474683058));
#18308=CARTESIAN_POINT('Ctrl Pts',(-1.12293169364966,3.20833333333333,1.94497474683058));
#18309=CARTESIAN_POINT('Ctrl Pts',(-1.68439754047449,3.26666666666666,0.972487373415292));
#18310=CARTESIAN_POINT('Ctrl Pts',(-2.24586338729932,3.32499999999999,1.37519470428917E-16));
#18311=CARTESIAN_POINT('Ctrl Pts',(-1.68439754047449,3.38333333333333,-0.972487373415291));
#18312=CARTESIAN_POINT('Ctrl Pts',(-1.12293169364966,3.44166666666666,-1.94497474683058));
#18313=CARTESIAN_POINT('Ctrl Pts',(-2.38190709812851E-16,3.49999999999999,
-1.94497474683058));
#18314=CARTESIAN_POINT('Ctrl Pts',(1.12293169364966,3.55833333333333,-1.94497474683058));
#18315=CARTESIAN_POINT('Ctrl Pts',(1.68439754047449,3.61666666666666,-0.972487373415292));
#18316=CARTESIAN_POINT('Ctrl Pts',(2.24586338729932,3.67499999999999,-4.12558411286752E-16));
#18317=CARTESIAN_POINT('Ctrl Pts',(1.68439754047449,3.73333333333333,0.97248737341529));
#18318=CARTESIAN_POINT('Ctrl Pts',(1.12293169364966,3.79166666666666,1.94497474683058));
#18319=CARTESIAN_POINT('Ctrl Pts',(0.,3.84999999999999,1.94497474683058));
#18320=CARTESIAN_POINT('Ctrl Pts',(-1.12293169364966,3.90833333333333,1.94497474683058));
#18321=CARTESIAN_POINT('Ctrl Pts',(-1.68439754047449,3.96666666666666,0.972487373415292));
#18322=CARTESIAN_POINT('Ctrl Pts',(-2.24586338729932,4.02499999999999,1.37519470428917E-16));
#18323=CARTESIAN_POINT('Ctrl Pts',(-1.68439754047449,4.08333333333333,-0.972487373415291));
#18324=CARTESIAN_POINT('Ctrl Pts',(-1.12293169364966,4.14166666666666,-1.94497474683058));
#18325=CARTESIAN_POINT('Ctrl Pts',(-2.38190709812851E-16,4.19999999999999,
-1.94497474683058));
#18326=CARTESIAN_POINT('Ctrl Pts',(1.12293169364966,4.25833333333332,-1.94497474683058));
#18327=CARTESIAN_POINT('Ctrl Pts',(1.68439754047449,4.31666666666666,-0.972487373415292));
#18328=CARTESIAN_POINT('Ctrl Pts',(2.24586338729932,4.37499999999999,-4.12558411286752E-16));
#18329=CARTESIAN_POINT('Ctrl Pts',(1.68439754047449,4.43333333333332,0.97248737341529));
#18330=CARTESIAN_POINT('Ctrl Pts',(1.12293169364966,4.49166666666666,1.94497474683058));
#18331=CARTESIAN_POINT('Ctrl Pts',(0.,4.54999999999999,1.94497474683058));
#18332=CARTESIAN_POINT('Ctrl Pts',(0.,0.35,2.15));
#18333=CARTESIAN_POINT('Ctrl Pts',(-1.2413030787577,0.408333333333333,2.15));
#18334=CARTESIAN_POINT('Ctrl Pts',(-1.86195461813654,0.466666666666667,
1.075));
#18335=CARTESIAN_POINT('Ctrl Pts',(-2.48260615751539,0.525,1.52015784217237E-16));
#18336=CARTESIAN_POINT('Ctrl Pts',(-1.86195461813654,0.583333333333333,
-1.075));
#18337=CARTESIAN_POINT('Ctrl Pts',(-1.2413030787577,0.641666666666666,-2.15));
#18338=CARTESIAN_POINT('Ctrl Pts',(-2.63299061816681E-16,0.699999999999999,
-2.15));
#18339=CARTESIAN_POINT('Ctrl Pts',(1.24130307875769,0.758333333333333,-2.15));
#18340=CARTESIAN_POINT('Ctrl Pts',(1.86195461813654,0.816666666666666,-1.075));
#18341=CARTESIAN_POINT('Ctrl Pts',(2.48260615751539,0.874999999999999,-4.5604735265171E-16));
#18342=CARTESIAN_POINT('Ctrl Pts',(1.86195461813654,0.933333333333332,1.075));
#18343=CARTESIAN_POINT('Ctrl Pts',(1.2413030787577,0.991666666666666,2.15));
#18344=CARTESIAN_POINT('Ctrl Pts',(0.,1.05,2.15));
#18345=CARTESIAN_POINT('Ctrl Pts',(-1.2413030787577,1.10833333333333,2.15));
#18346=CARTESIAN_POINT('Ctrl Pts',(-1.86195461813654,1.16666666666667,1.075));
#18347=CARTESIAN_POINT('Ctrl Pts',(-2.48260615751539,1.225,1.52015784217237E-16));
#18348=CARTESIAN_POINT('Ctrl Pts',(-1.86195461813654,1.28333333333333,-1.075));
#18349=CARTESIAN_POINT('Ctrl Pts',(-1.2413030787577,1.34166666666666,-2.15));
#18350=CARTESIAN_POINT('Ctrl Pts',(-2.63299061816681E-16,1.4,-2.15));
#18351=CARTESIAN_POINT('Ctrl Pts',(1.24130307875769,1.45833333333333,-2.15));
#18352=CARTESIAN_POINT('Ctrl Pts',(1.86195461813654,1.51666666666666,-1.075));
#18353=CARTESIAN_POINT('Ctrl Pts',(2.48260615751539,1.575,-4.5604735265171E-16));
#18354=CARTESIAN_POINT('Ctrl Pts',(1.86195461813654,1.63333333333333,1.075));
#18355=CARTESIAN_POINT('Ctrl Pts',(1.2413030787577,1.69166666666666,2.15));
#18356=CARTESIAN_POINT('Ctrl Pts',(0.,1.75,2.15));
#18357=CARTESIAN_POINT('Ctrl Pts',(-1.2413030787577,1.80833333333333,2.15));
#18358=CARTESIAN_POINT('Ctrl Pts',(-1.86195461813654,1.86666666666666,1.075));
#18359=CARTESIAN_POINT('Ctrl Pts',(-2.48260615751539,1.925,1.52015784217237E-16));
#18360=CARTESIAN_POINT('Ctrl Pts',(-1.86195461813654,1.98333333333333,-1.075));
#18361=CARTESIAN_POINT('Ctrl Pts',(-1.2413030787577,2.04166666666666,-2.15));
#18362=CARTESIAN_POINT('Ctrl Pts',(-2.63299061816681E-16,2.1,-2.15));
#18363=CARTESIAN_POINT('Ctrl Pts',(1.24130307875769,2.15833333333333,-2.15));
#18364=CARTESIAN_POINT('Ctrl Pts',(1.86195461813654,2.21666666666666,-1.075));
#18365=CARTESIAN_POINT('Ctrl Pts',(2.48260615751539,2.275,-4.5604735265171E-16));
#18366=CARTESIAN_POINT('Ctrl Pts',(1.86195461813654,2.33333333333333,1.075));
#18367=CARTESIAN_POINT('Ctrl Pts',(1.2413030787577,2.39166666666666,2.15));
#18368=CARTESIAN_POINT('Ctrl Pts',(0.,2.45,2.15));
#18369=CARTESIAN_POINT('Ctrl Pts',(-1.2413030787577,2.50833333333333,2.15));
#18370=CARTESIAN_POINT('Ctrl Pts',(-1.86195461813654,2.56666666666666,1.075));
#18371=CARTESIAN_POINT('Ctrl Pts',(-2.48260615751539,2.625,1.52015784217237E-16));
#18372=CARTESIAN_POINT('Ctrl Pts',(-1.86195461813654,2.68333333333333,-1.075));
#18373=CARTESIAN_POINT('Ctrl Pts',(-1.2413030787577,2.74166666666666,-2.15));
#18374=CARTESIAN_POINT('Ctrl Pts',(-2.63299061816681E-16,2.8,-2.15));
#18375=CARTESIAN_POINT('Ctrl Pts',(1.24130307875769,2.85833333333333,-2.15));
#18376=CARTESIAN_POINT('Ctrl Pts',(1.86195461813654,2.91666666666666,-1.075));
#18377=CARTESIAN_POINT('Ctrl Pts',(2.48260615751539,2.97499999999999,-4.5604735265171E-16));
#18378=CARTESIAN_POINT('Ctrl Pts',(1.86195461813654,3.03333333333333,1.075));
#18379=CARTESIAN_POINT('Ctrl Pts',(1.2413030787577,3.09166666666666,2.15));
#18380=CARTESIAN_POINT('Ctrl Pts',(0.,3.15,2.15));
#18381=CARTESIAN_POINT('Ctrl Pts',(-1.2413030787577,3.20833333333333,2.15));
#18382=CARTESIAN_POINT('Ctrl Pts',(-1.86195461813654,3.26666666666666,1.075));
#18383=CARTESIAN_POINT('Ctrl Pts',(-2.48260615751539,3.32499999999999,1.52015784217237E-16));
#18384=CARTESIAN_POINT('Ctrl Pts',(-1.86195461813654,3.38333333333333,-1.075));
#18385=CARTESIAN_POINT('Ctrl Pts',(-1.2413030787577,3.44166666666666,-2.15));
#18386=CARTESIAN_POINT('Ctrl Pts',(-2.63299061816681E-16,3.49999999999999,
-2.15));
#18387=CARTESIAN_POINT('Ctrl Pts',(1.24130307875769,3.55833333333333,-2.15));
#18388=CARTESIAN_POINT('Ctrl Pts',(1.86195461813654,3.61666666666666,-1.075));
#18389=CARTESIAN_POINT('Ctrl Pts',(2.48260615751539,3.67499999999999,-4.5604735265171E-16));
#18390=CARTESIAN_POINT('Ctrl Pts',(1.86195461813654,3.73333333333333,1.075));
#18391=CARTESIAN_POINT('Ctrl Pts',(1.2413030787577,3.79166666666666,2.15));
#18392=CARTESIAN_POINT('Ctrl Pts',(0.,3.84999999999999,2.15));
#18393=CARTESIAN_POINT('Ctrl Pts',(-1.2413030787577,3.90833333333333,2.15));
#18394=CARTESIAN_POINT('Ctrl Pts',(-1.86195461813654,3.96666666666666,1.075));
#18395=CARTESIAN_POINT('Ctrl Pts',(-2.48260615751539,4.02499999999999,1.52015784217237E-16));
#18396=CARTESIAN_POINT('Ctrl Pts',(-1.86195461813654,4.08333333333333,-1.075));
#18397=CARTESIAN_POINT('Ctrl Pts',(-1.2413030787577,4.14166666666666,-2.15));
#18398=CARTESIAN_POINT('Ctrl Pts',(-2.63299061816681E-16,4.19999999999999,
-2.15));
#18399=CARTESIAN_POINT('Ctrl Pts',(1.24130307875769,4.25833333333333,-2.15));
#18400=CARTESIAN_POINT('Ctrl Pts',(1.86195461813654,4.31666666666666,-1.075));
#18401=CARTESIAN_POINT('Ctrl Pts',(2.48260615751539,4.37499999999999,-4.5604735265171E-16));
#18402=CARTESIAN_POINT('Ctrl Pts',(1.86195461813654,4.43333333333333,1.075));
#18403=CARTESIAN_POINT('Ctrl Pts',(1.2413030787577,4.49166666666666,2.15));
#18404=CARTESIAN_POINT('Ctrl Pts',(0.,4.54999999999999,2.15));
#18405=CARTESIAN_POINT('',(-7.40933783759325E-14,4.2,1.8));
#18406=CARTESIAN_POINT('',(-8.82371251094361E-14,4.55,2.15));
#18407=CARTESIAN_POINT('Origin',(-1.80160437084306E-13,4.2,2.15));
#18408=CARTESIAN_POINT('',(-8.87637232330694E-14,3.85,2.15));
#18409=CARTESIAN_POINT('Ctrl Pts',(1.05346240894046E-14,3.84999999999999,
2.15));
#18410=CARTESIAN_POINT('Ctrl Pts',(-1.24130307875769,3.90833333333333,2.15));
#18411=CARTESIAN_POINT('Ctrl Pts',(-1.86195461813654,3.96666666666666,1.075));
#18412=CARTESIAN_POINT('Ctrl Pts',(-2.48260615751539,4.02499999999999,1.67263463193154E-14));
#18413=CARTESIAN_POINT('Ctrl Pts',(-1.86195461813655,4.08333333333333,-1.07499999999999));
#18414=CARTESIAN_POINT('Ctrl Pts',(-1.2413030787577,4.14166666666666,-2.15));
#18415=CARTESIAN_POINT('Ctrl Pts',(-1.07979231512212E-14,4.19999999999999,
-2.15));
#18416=CARTESIAN_POINT('Ctrl Pts',(1.24130307875769,4.25833333333332,-2.15));
#18417=CARTESIAN_POINT('Ctrl Pts',(1.86195461813654,4.31666666666666,-1.07500000000001));
#18418=CARTESIAN_POINT('Ctrl Pts',(2.48260615751539,4.37499999999999,-8.21038903287055E-15));
#18419=CARTESIAN_POINT('Ctrl Pts',(1.86195461813655,4.43333333333332,1.07499999999999));
#18420=CARTESIAN_POINT('Ctrl Pts',(1.24130307875771,4.49166666666666,2.14999999999999));
#18421=CARTESIAN_POINT('Ctrl Pts',(-8.82371251094361E-14,4.55,2.15));
#18422=CARTESIAN_POINT('',(2.63299061816681E-16,0.349999999999999,2.15));
#18423=CARTESIAN_POINT('Ctrl Pts',(2.63299061816681E-16,0.349999999999999,
2.15));
#18424=CARTESIAN_POINT('Ctrl Pts',(-1.24130307875769,0.408333333333333,
2.15));
#18425=CARTESIAN_POINT('Ctrl Pts',(-1.86195461813654,0.466666666666666,
1.075));
#18426=CARTESIAN_POINT('Ctrl Pts',(-2.48260615751539,0.524999999999999,
4.5604735265171E-16));
#18427=CARTESIAN_POINT('Ctrl Pts',(-1.86195461813654,0.583333333333332,
-1.075));
#18428=CARTESIAN_POINT('Ctrl Pts',(-1.2413030787577,0.641666666666665,-2.15));
#18429=CARTESIAN_POINT('Ctrl Pts',(-5.26598123633362E-16,0.699999999999999,
-2.15));
#18430=CARTESIAN_POINT('Ctrl Pts',(1.24130307875769,0.758333333333332,-2.15));
#18431=CARTESIAN_POINT('Ctrl Pts',(1.86195461813654,0.816666666666665,-1.075));
#18432=CARTESIAN_POINT('Ctrl Pts',(2.48260615751539,0.874999999999999,-7.60078921086183E-16));
#18433=CARTESIAN_POINT('Ctrl Pts',(1.86195461813654,0.933333333333332,1.075));
#18434=CARTESIAN_POINT('Ctrl Pts',(1.2413030787577,0.991666666666665,2.15));
#18435=CARTESIAN_POINT('Ctrl Pts',(7.89897185450043E-16,1.05,2.15));
#18436=CARTESIAN_POINT('Ctrl Pts',(-1.24130307875769,1.10833333333333,2.15));
#18437=CARTESIAN_POINT('Ctrl Pts',(-1.86195461813654,1.16666666666666,1.075));
#18438=CARTESIAN_POINT('Ctrl Pts',(-2.48260615751539,1.225,3.26910770324048E-15));
#18439=CARTESIAN_POINT('Ctrl Pts',(-1.86195461813654,1.28333333333333,-1.075));
#18440=CARTESIAN_POINT('Ctrl Pts',(-1.2413030787577,1.34166666666666,-2.15));
#18441=CARTESIAN_POINT('Ctrl Pts',(-1.05319624726672E-15,1.4,-2.15));
#18442=CARTESIAN_POINT('Ctrl Pts',(1.24130307875769,1.45833333333333,-2.15));
#18443=CARTESIAN_POINT('Ctrl Pts',(1.86195461813654,1.51666666666666,-1.075));
#18444=CARTESIAN_POINT('Ctrl Pts',(2.48260615751539,1.575,-1.36814205795513E-15));
#18445=CARTESIAN_POINT('Ctrl Pts',(1.86195461813654,1.63333333333333,1.075));
#18446=CARTESIAN_POINT('Ctrl Pts',(1.2413030787577,1.69166666666666,2.15));
#18447=CARTESIAN_POINT('Ctrl Pts',(1.3164953090834E-15,1.75,2.15));
#18448=CARTESIAN_POINT('Ctrl Pts',(-1.24130307875769,1.80833333333333,2.15));
#18449=CARTESIAN_POINT('Ctrl Pts',(-1.86195461813654,1.86666666666666,1.075));
#18450=CARTESIAN_POINT('Ctrl Pts',(-2.48260615751539,1.925,6.08216805382924E-15));
#18451=CARTESIAN_POINT('Ctrl Pts',(-1.86195461813654,1.98333333333333,-1.075));
#18452=CARTESIAN_POINT('Ctrl Pts',(-1.2413030787577,2.04166666666666,-2.15));
#18453=CARTESIAN_POINT('Ctrl Pts',(-5.39896157561062E-15,2.1,-2.15));
#18454=CARTESIAN_POINT('Ctrl Pts',(1.24130307875769,2.15833333333333,-2.15));
#18455=CARTESIAN_POINT('Ctrl Pts',(1.86195461813654,2.21666666666666,-1.075));
#18456=CARTESIAN_POINT('Ctrl Pts',(2.48260615751539,2.275,-6.38619962226372E-15));
#18457=CARTESIAN_POINT('Ctrl Pts',(1.86195461813655,2.33333333333333,1.07499999999999));
#18458=CARTESIAN_POINT('Ctrl Pts',(1.2413030787577,2.39166666666666,2.15));
#18459=CARTESIAN_POINT('Ctrl Pts',(1.84309343271677E-15,2.45,2.15));
#18460=CARTESIAN_POINT('Ctrl Pts',(-1.24130307875769,2.50833333333333,2.15));
#18461=CARTESIAN_POINT('Ctrl Pts',(-1.86195461813654,2.56666666666666,1.075));
#18462=CARTESIAN_POINT('Ctrl Pts',(-2.48260615751539,2.62499999999999,6.69023119069819E-15));
#18463=CARTESIAN_POINT('Ctrl Pts',(-1.86195461813655,2.68333333333333,-1.07499999999999));
#18464=CARTESIAN_POINT('Ctrl Pts',(-1.2413030787577,2.74166666666666,-2.14999999999999));
#18465=CARTESIAN_POINT('Ctrl Pts',(-2.10639249453345E-15,2.79999999999999,
-2.15));
#18466=CARTESIAN_POINT('Ctrl Pts',(1.24130307875769,2.85833333333333,-2.15));
#18467=CARTESIAN_POINT('Ctrl Pts',(1.86195461813654,2.91666666666666,-1.075));
#18468=CARTESIAN_POINT('Ctrl Pts',(2.48260615751539,2.97499999999999,-6.99426275913266E-15));
#18469=CARTESIAN_POINT('Ctrl Pts',(1.86195461813655,3.03333333333333,1.07499999999999));
#18470=CARTESIAN_POINT('Ctrl Pts',(1.2413030787577,3.09166666666666,2.14999999999999));
#18471=CARTESIAN_POINT('Ctrl Pts',(2.36969155635013E-15,3.14999999999999,
2.15));
#18472=CARTESIAN_POINT('Ctrl Pts',(-1.24130307875769,3.20833333333333,2.15));
#18473=CARTESIAN_POINT('Ctrl Pts',(-1.86195461813654,3.26666666666666,1.075));
#18474=CARTESIAN_POINT('Ctrl Pts',(-2.48260615751539,3.32499999999999,7.29829432756713E-15));
#18475=CARTESIAN_POINT('Ctrl Pts',(-1.86195461813655,3.38333333333333,-1.07499999999999));
#18476=CARTESIAN_POINT('Ctrl Pts',(-1.2413030787577,3.44166666666666,-2.14999999999999));
#18477=CARTESIAN_POINT('Ctrl Pts',(-1.02713250275879E-14,3.49999999999999,
-2.15));
#18478=CARTESIAN_POINT('Ctrl Pts',(1.24130307875769,3.55833333333333,-2.15));
#18479=CARTESIAN_POINT('Ctrl Pts',(1.86195461813654,3.61666666666666,-1.075));
#18480=CARTESIAN_POINT('Ctrl Pts',(2.48260615751539,3.67499999999999,-7.60232589600161E-15));
#18481=CARTESIAN_POINT('Ctrl Pts',(1.86195461813655,3.73333333333333,1.07499999999999));
#18482=CARTESIAN_POINT('Ctrl Pts',(1.2413030787577,3.79166666666666,2.14999999999999));
#18483=CARTESIAN_POINT('Ctrl Pts',(1.05346240894046E-14,3.84999999999999,
2.15));
#18484=CARTESIAN_POINT('',(0.,0.,1.8));
#18485=CARTESIAN_POINT('Origin',(0.,0.,2.15));
#18486=CARTESIAN_POINT('Ctrl Pts',(0.,0.,1.8));
#18487=CARTESIAN_POINT('Ctrl Pts',(-1.03923048454133,0.0583333333333332,
1.8));
#18488=CARTESIAN_POINT('Ctrl Pts',(-1.55884572681199,0.116666666666666,
0.9));
#18489=CARTESIAN_POINT('Ctrl Pts',(-2.07846096908265,0.175,1.27269028646989E-16));
#18490=CARTESIAN_POINT('Ctrl Pts',(-1.55884572681199,0.233333333333333,
-0.9));
#18491=CARTESIAN_POINT('Ctrl Pts',(-1.03923048454133,0.291666666666666,
-1.8));
#18492=CARTESIAN_POINT('Ctrl Pts',(-2.20436423846524E-16,0.349999999999999,
-1.8));
#18493=CARTESIAN_POINT('Ctrl Pts',(1.03923048454133,0.408333333333333,-1.8));
#18494=CARTESIAN_POINT('Ctrl Pts',(1.55884572681199,0.466666666666666,-0.900000000000001));
#18495=CARTESIAN_POINT('Ctrl Pts',(2.07846096908265,0.524999999999999,-3.81807085940967E-16));
#18496=CARTESIAN_POINT('Ctrl Pts',(1.55884572681199,0.583333333333332,0.899999999999999));
#18497=CARTESIAN_POINT('Ctrl Pts',(1.03923048454133,0.641666666666665,1.8));
#18498=CARTESIAN_POINT('Ctrl Pts',(4.40872847693047E-16,0.699999999999999,
1.8));
#18499=CARTESIAN_POINT('Ctrl Pts',(-1.03923048454132,0.758333333333332,
1.8));
#18500=CARTESIAN_POINT('Ctrl Pts',(-1.55884572681199,0.816666666666665,
0.900000000000001));
#18501=CARTESIAN_POINT('Ctrl Pts',(-2.07846096908265,0.874999999999998,
2.48238932216317E-15));
#18502=CARTESIAN_POINT('Ctrl Pts',(-1.55884572681199,0.933333333333332,
-0.899999999999999));
#18503=CARTESIAN_POINT('Ctrl Pts',(-1.03923048454133,0.991666666666665,
-1.8));
#18504=CARTESIAN_POINT('Ctrl Pts',(-6.61309271539571E-16,1.05,-1.8));
#18505=CARTESIAN_POINT('Ctrl Pts',(1.03923048454132,1.10833333333333,-1.8));
#18506=CARTESIAN_POINT('Ctrl Pts',(1.55884572681199,1.16666666666666,-0.900000000000002));
#18507=CARTESIAN_POINT('Ctrl Pts',(2.07846096908265,1.225,-8.90883200528922E-16));
#18508=CARTESIAN_POINT('Ctrl Pts',(1.55884572681199,1.28333333333333,0.899999999999998));
#18509=CARTESIAN_POINT('Ctrl Pts',(1.03923048454133,1.34166666666666,1.8));
#18510=CARTESIAN_POINT('Ctrl Pts',(8.81745695386094E-16,1.4,1.8));
#18511=CARTESIAN_POINT('Ctrl Pts',(-1.03923048454132,1.45833333333333,1.8));
#18512=CARTESIAN_POINT('Ctrl Pts',(-1.55884572681199,1.51666666666666,0.900000000000003));
#18513=CARTESIAN_POINT('Ctrl Pts',(-2.07846096908265,1.575,4.83750961567934E-15));
#18514=CARTESIAN_POINT('Ctrl Pts',(-1.55884572681199,1.63333333333333,-0.899999999999998));
#18515=CARTESIAN_POINT('Ctrl Pts',(-1.03923048454133,1.69166666666666,-1.8));
#18516=CARTESIAN_POINT('Ctrl Pts',(-4.29962443015307E-15,1.75,-1.8));
#18517=CARTESIAN_POINT('Ctrl Pts',(1.03923048454132,1.80833333333333,-1.8));
#18518=CARTESIAN_POINT('Ctrl Pts',(1.55884572681199,1.86666666666666,-0.900000000000003));
#18519=CARTESIAN_POINT('Ctrl Pts',(2.07846096908265,1.925,-5.09204767297332E-15));
#18520=CARTESIAN_POINT('Ctrl Pts',(1.55884572681199,1.98333333333333,0.899999999999995));
#18521=CARTESIAN_POINT('Ctrl Pts',(1.03923048454133,2.04166666666666,1.8));
#18522=CARTESIAN_POINT('Ctrl Pts',(1.32261854307914E-15,2.1,1.8));
#18523=CARTESIAN_POINT('Ctrl Pts',(-1.03923048454132,2.15833333333333,1.8));
#18524=CARTESIAN_POINT('Ctrl Pts',(-1.55884572681199,2.21666666666666,0.900000000000003));
#18525=CARTESIAN_POINT('Ctrl Pts',(-2.07846096908265,2.275,5.3465857302673E-15));
#18526=CARTESIAN_POINT('Ctrl Pts',(-1.55884572681199,2.33333333333333,-0.899999999999995));
#18527=CARTESIAN_POINT('Ctrl Pts',(-1.03923048454133,2.39166666666666,-1.8));
#18528=CARTESIAN_POINT('Ctrl Pts',(-1.54305496692567E-15,2.45,-1.8));
#18529=CARTESIAN_POINT('Ctrl Pts',(1.03923048454132,2.50833333333333,-1.8));
#18530=CARTESIAN_POINT('Ctrl Pts',(1.55884572681199,2.56666666666666,-0.900000000000003));
#18531=CARTESIAN_POINT('Ctrl Pts',(2.07846096908265,2.625,-5.60112378756128E-15));
#18532=CARTESIAN_POINT('Ctrl Pts',(1.55884572681199,2.68333333333333,0.899999999999995));
#18533=CARTESIAN_POINT('Ctrl Pts',(1.03923048454133,2.74166666666666,1.8));
#18534=CARTESIAN_POINT('Ctrl Pts',(1.76349139077219E-15,2.79999999999999,
1.8));
#18535=CARTESIAN_POINT('Ctrl Pts',(-1.03923048454132,2.85833333333333,1.8));
#18536=CARTESIAN_POINT('Ctrl Pts',(-1.55884572681199,2.91666666666666,0.900000000000003));
#18537=CARTESIAN_POINT('Ctrl Pts',(-2.07846096908265,2.97499999999999,5.85566184485525E-15));
#18538=CARTESIAN_POINT('Ctrl Pts',(-1.55884572681199,3.03333333333333,-0.899999999999995));
#18539=CARTESIAN_POINT('Ctrl Pts',(-1.03923048454133,3.09166666666666,-1.8));
#18540=CARTESIAN_POINT('Ctrl Pts',(-8.37881243645961E-15,3.14999999999999,
-1.8));
#18541=CARTESIAN_POINT('Ctrl Pts',(1.03923048454132,3.20833333333333,-1.8));
#18542=CARTESIAN_POINT('Ctrl Pts',(1.55884572681199,3.26666666666666,-0.900000000000004));
#18543=CARTESIAN_POINT('Ctrl Pts',(2.07846096908265,3.32499999999999,-6.11019990214923E-15));
#18544=CARTESIAN_POINT('Ctrl Pts',(1.55884572681199,3.38333333333333,0.899999999999995));
#18545=CARTESIAN_POINT('Ctrl Pts',(1.03923048454133,3.44166666666666,1.8));
#18546=CARTESIAN_POINT('Ctrl Pts',(8.59924886030614E-15,3.49999999999999,
1.8));
#18547=CARTESIAN_POINT('Ctrl Pts',(-1.03923048454132,3.55833333333333,1.8));
#18548=CARTESIAN_POINT('Ctrl Pts',(-1.55884572681199,3.61666666666666,0.900000000000004));
#18549=CARTESIAN_POINT('Ctrl Pts',(-2.07846096908265,3.67499999999999,1.37489146751561E-14));
#18550=CARTESIAN_POINT('Ctrl Pts',(-1.55884572681199,3.73333333333333,-0.899999999999994));
#18551=CARTESIAN_POINT('Ctrl Pts',(-1.03923048454133,3.79166666666666,-1.8));
#18552=CARTESIAN_POINT('Ctrl Pts',(-8.81968528415266E-15,3.84999999999999,
-1.8));
#18553=CARTESIAN_POINT('Ctrl Pts',(1.03923048454132,3.90833333333333,-1.8));
#18554=CARTESIAN_POINT('Ctrl Pts',(1.55884572681198,3.96666666666666,-0.90000000000001));
#18555=CARTESIAN_POINT('Ctrl Pts',(2.07846096908265,4.02499999999999,-6.61927601673719E-15));
#18556=CARTESIAN_POINT('Ctrl Pts',(1.558845726812,4.08333333333333,0.899999999999989));
#18557=CARTESIAN_POINT('Ctrl Pts',(1.03923048454133,4.14166666666666,1.8));
#18558=CARTESIAN_POINT('Ctrl Pts',(-7.40933783759325E-14,4.2,1.8));
#18559=CARTESIAN_POINT('Ctrl Pts',(0.,-0.35,2.15));
#18560=CARTESIAN_POINT('Ctrl Pts',(-1.2413030787577,-0.291666666666667,
2.15));
#18561=CARTESIAN_POINT('Ctrl Pts',(-1.86195461813654,-0.233333333333334,
1.075));
#18562=CARTESIAN_POINT('Ctrl Pts',(-2.48260615751539,-0.175,1.52015784217237E-16));
#18563=CARTESIAN_POINT('Ctrl Pts',(-1.86195461813654,-0.116666666666667,
-1.075));
#18564=CARTESIAN_POINT('Ctrl Pts',(-1.2413030787577,-0.058333333333334,
-2.15));
#18565=CARTESIAN_POINT('Ctrl Pts',(-2.63299061816681E-16,-7.58941520739853E-16,
-2.15));
#18566=CARTESIAN_POINT('Ctrl Pts',(1.24130307875769,0.0583333333333325,
-2.15));
#18567=CARTESIAN_POINT('Ctrl Pts',(1.86195461813654,0.116666666666666,-1.075));
#18568=CARTESIAN_POINT('Ctrl Pts',(2.48260615751539,0.174999999999999,-4.5604735265171E-16));
#18569=CARTESIAN_POINT('Ctrl Pts',(1.86195461813654,0.233333333333332,1.075));
#18570=CARTESIAN_POINT('Ctrl Pts',(1.2413030787577,0.291666666666665,2.15));
#18571=CARTESIAN_POINT('Ctrl Pts',(0.,0.349999999999999,2.15));
#18572=CARTESIAN_POINT('Ctrl Pts',(-1.2413030787577,0.408333333333332,2.15));
#18573=CARTESIAN_POINT('Ctrl Pts',(-1.86195461813654,0.466666666666665,
1.075));
#18574=CARTESIAN_POINT('Ctrl Pts',(-2.48260615751539,0.524999999999998,
1.52015784217237E-16));
#18575=CARTESIAN_POINT('Ctrl Pts',(-1.86195461813654,0.583333333333331,
-1.075));
#18576=CARTESIAN_POINT('Ctrl Pts',(-1.2413030787577,0.641666666666665,-2.15));
#18577=CARTESIAN_POINT('Ctrl Pts',(-2.63299061816681E-16,0.699999999999998,
-2.15));
#18578=CARTESIAN_POINT('Ctrl Pts',(1.24130307875769,0.758333333333331,-2.15));
#18579=CARTESIAN_POINT('Ctrl Pts',(1.86195461813654,0.816666666666664,-1.075));
#18580=CARTESIAN_POINT('Ctrl Pts',(2.48260615751539,0.874999999999997,-4.5604735265171E-16));
#18581=CARTESIAN_POINT('Ctrl Pts',(1.86195461813654,0.933333333333331,1.075));
#18582=CARTESIAN_POINT('Ctrl Pts',(1.2413030787577,0.991666666666664,2.15));
#18583=CARTESIAN_POINT('Ctrl Pts',(0.,1.05,2.15));
#18584=CARTESIAN_POINT('Ctrl Pts',(-1.2413030787577,1.10833333333333,2.15));
#18585=CARTESIAN_POINT('Ctrl Pts',(-1.86195461813654,1.16666666666666,1.075));
#18586=CARTESIAN_POINT('Ctrl Pts',(-2.48260615751539,1.225,1.52015784217237E-16));
#18587=CARTESIAN_POINT('Ctrl Pts',(-1.86195461813654,1.28333333333333,-1.075));
#18588=CARTESIAN_POINT('Ctrl Pts',(-1.2413030787577,1.34166666666666,-2.15));
#18589=CARTESIAN_POINT('Ctrl Pts',(-2.63299061816681E-16,1.4,-2.15));
#18590=CARTESIAN_POINT('Ctrl Pts',(1.24130307875769,1.45833333333333,-2.15));
#18591=CARTESIAN_POINT('Ctrl Pts',(1.86195461813654,1.51666666666666,-1.075));
#18592=CARTESIAN_POINT('Ctrl Pts',(2.48260615751539,1.575,-4.5604735265171E-16));
#18593=CARTESIAN_POINT('Ctrl Pts',(1.86195461813654,1.63333333333333,1.075));
#18594=CARTESIAN_POINT('Ctrl Pts',(1.2413030787577,1.69166666666666,2.15));
#18595=CARTESIAN_POINT('Ctrl Pts',(0.,1.75,2.15));
#18596=CARTESIAN_POINT('Ctrl Pts',(-1.2413030787577,1.80833333333333,2.15));
#18597=CARTESIAN_POINT('Ctrl Pts',(-1.86195461813654,1.86666666666666,1.075));
#18598=CARTESIAN_POINT('Ctrl Pts',(-2.48260615751539,1.925,1.52015784217237E-16));
#18599=CARTESIAN_POINT('Ctrl Pts',(-1.86195461813654,1.98333333333333,-1.075));
#18600=CARTESIAN_POINT('Ctrl Pts',(-1.2413030787577,2.04166666666666,-2.15));
#18601=CARTESIAN_POINT('Ctrl Pts',(-2.63299061816681E-16,2.1,-2.15));
#18602=CARTESIAN_POINT('Ctrl Pts',(1.24130307875769,2.15833333333333,-2.15));
#18603=CARTESIAN_POINT('Ctrl Pts',(1.86195461813654,2.21666666666666,-1.075));
#18604=CARTESIAN_POINT('Ctrl Pts',(2.48260615751539,2.275,-4.5604735265171E-16));
#18605=CARTESIAN_POINT('Ctrl Pts',(1.86195461813654,2.33333333333333,1.075));
#18606=CARTESIAN_POINT('Ctrl Pts',(1.2413030787577,2.39166666666666,2.15));
#18607=CARTESIAN_POINT('Ctrl Pts',(0.,2.44999999999999,2.15));
#18608=CARTESIAN_POINT('Ctrl Pts',(-1.2413030787577,2.50833333333333,2.15));
#18609=CARTESIAN_POINT('Ctrl Pts',(-1.86195461813654,2.56666666666666,1.075));
#18610=CARTESIAN_POINT('Ctrl Pts',(-2.48260615751539,2.62499999999999,1.52015784217237E-16));
#18611=CARTESIAN_POINT('Ctrl Pts',(-1.86195461813654,2.68333333333333,-1.075));
#18612=CARTESIAN_POINT('Ctrl Pts',(-1.2413030787577,2.74166666666666,-2.15));
#18613=CARTESIAN_POINT('Ctrl Pts',(-2.63299061816681E-16,2.79999999999999,
-2.15));
#18614=CARTESIAN_POINT('Ctrl Pts',(1.24130307875769,2.85833333333333,-2.15));
#18615=CARTESIAN_POINT('Ctrl Pts',(1.86195461813654,2.91666666666666,-1.075));
#18616=CARTESIAN_POINT('Ctrl Pts',(2.48260615751539,2.97499999999999,-4.5604735265171E-16));
#18617=CARTESIAN_POINT('Ctrl Pts',(1.86195461813654,3.03333333333333,1.075));
#18618=CARTESIAN_POINT('Ctrl Pts',(1.2413030787577,3.09166666666666,2.15));
#18619=CARTESIAN_POINT('Ctrl Pts',(0.,3.14999999999999,2.15));
#18620=CARTESIAN_POINT('Ctrl Pts',(-1.2413030787577,3.20833333333333,2.15));
#18621=CARTESIAN_POINT('Ctrl Pts',(-1.86195461813654,3.26666666666666,1.075));
#18622=CARTESIAN_POINT('Ctrl Pts',(-2.48260615751539,3.32499999999999,1.52015784217237E-16));
#18623=CARTESIAN_POINT('Ctrl Pts',(-1.86195461813654,3.38333333333333,-1.075));
#18624=CARTESIAN_POINT('Ctrl Pts',(-1.2413030787577,3.44166666666666,-2.15));
#18625=CARTESIAN_POINT('Ctrl Pts',(-2.63299061816681E-16,3.49999999999999,
-2.15));
#18626=CARTESIAN_POINT('Ctrl Pts',(1.24130307875769,3.55833333333333,-2.15));
#18627=CARTESIAN_POINT('Ctrl Pts',(1.86195461813654,3.61666666666666,-1.075));
#18628=CARTESIAN_POINT('Ctrl Pts',(2.48260615751539,3.67499999999999,-4.5604735265171E-16));
#18629=CARTESIAN_POINT('Ctrl Pts',(1.86195461813654,3.73333333333333,1.075));
#18630=CARTESIAN_POINT('Ctrl Pts',(1.2413030787577,3.79166666666666,2.15));
#18631=CARTESIAN_POINT('Ctrl Pts',(0.,3.84999999999999,2.15));
#18632=CARTESIAN_POINT('Ctrl Pts',(0.,-0.35,1.94497474683058));
#18633=CARTESIAN_POINT('Ctrl Pts',(-1.12293169364966,-0.291666666666667,
1.94497474683058));
#18634=CARTESIAN_POINT('Ctrl Pts',(-1.68439754047449,-0.233333333333334,
0.972487373415292));
#18635=CARTESIAN_POINT('Ctrl Pts',(-2.24586338729932,-0.175,1.37519470428917E-16));
#18636=CARTESIAN_POINT('Ctrl Pts',(-1.68439754047449,-0.116666666666667,
-0.972487373415291));
#18637=CARTESIAN_POINT('Ctrl Pts',(-1.12293169364966,-0.058333333333334,
-1.94497474683058));
#18638=CARTESIAN_POINT('Ctrl Pts',(-2.38190709812851E-16,-8.13151629364128E-16,
-1.94497474683058));
#18639=CARTESIAN_POINT('Ctrl Pts',(1.12293169364966,0.0583333333333324,
-1.94497474683058));
#18640=CARTESIAN_POINT('Ctrl Pts',(1.68439754047449,0.116666666666666,-0.972487373415292));
#18641=CARTESIAN_POINT('Ctrl Pts',(2.24586338729932,0.174999999999999,-4.12558411286752E-16));
#18642=CARTESIAN_POINT('Ctrl Pts',(1.68439754047449,0.233333333333332,0.97248737341529));
#18643=CARTESIAN_POINT('Ctrl Pts',(1.12293169364966,0.291666666666665,1.94497474683058));
#18644=CARTESIAN_POINT('Ctrl Pts',(0.,0.349999999999998,1.94497474683058));
#18645=CARTESIAN_POINT('Ctrl Pts',(-1.12293169364966,0.408333333333332,
1.94497474683058));
#18646=CARTESIAN_POINT('Ctrl Pts',(-1.68439754047449,0.466666666666665,
0.972487373415292));
#18647=CARTESIAN_POINT('Ctrl Pts',(-2.24586338729932,0.524999999999998,
1.37519470428917E-16));
#18648=CARTESIAN_POINT('Ctrl Pts',(-1.68439754047449,0.583333333333331,
-0.972487373415291));
#18649=CARTESIAN_POINT('Ctrl Pts',(-1.12293169364966,0.641666666666665,
-1.94497474683058));
#18650=CARTESIAN_POINT('Ctrl Pts',(-2.38190709812851E-16,0.699999999999998,
-1.94497474683058));
#18651=CARTESIAN_POINT('Ctrl Pts',(1.12293169364966,0.758333333333331,-1.94497474683058));
#18652=CARTESIAN_POINT('Ctrl Pts',(1.68439754047449,0.816666666666664,-0.972487373415292));
#18653=CARTESIAN_POINT('Ctrl Pts',(2.24586338729932,0.874999999999998,-4.12558411286752E-16));
#18654=CARTESIAN_POINT('Ctrl Pts',(1.68439754047449,0.933333333333331,0.97248737341529));
#18655=CARTESIAN_POINT('Ctrl Pts',(1.12293169364966,0.991666666666664,1.94497474683058));
#18656=CARTESIAN_POINT('Ctrl Pts',(0.,1.05,1.94497474683058));
#18657=CARTESIAN_POINT('Ctrl Pts',(-1.12293169364966,1.10833333333333,1.94497474683058));
#18658=CARTESIAN_POINT('Ctrl Pts',(-1.68439754047449,1.16666666666666,0.972487373415292));
#18659=CARTESIAN_POINT('Ctrl Pts',(-2.24586338729932,1.225,1.37519470428917E-16));
#18660=CARTESIAN_POINT('Ctrl Pts',(-1.68439754047449,1.28333333333333,-0.972487373415291));
#18661=CARTESIAN_POINT('Ctrl Pts',(-1.12293169364966,1.34166666666666,-1.94497474683058));
#18662=CARTESIAN_POINT('Ctrl Pts',(-2.38190709812851E-16,1.4,-1.94497474683058));
#18663=CARTESIAN_POINT('Ctrl Pts',(1.12293169364966,1.45833333333333,-1.94497474683058));
#18664=CARTESIAN_POINT('Ctrl Pts',(1.68439754047449,1.51666666666666,-0.972487373415292));
#18665=CARTESIAN_POINT('Ctrl Pts',(2.24586338729932,1.575,-4.12558411286752E-16));
#18666=CARTESIAN_POINT('Ctrl Pts',(1.68439754047449,1.63333333333333,0.97248737341529));
#18667=CARTESIAN_POINT('Ctrl Pts',(1.12293169364966,1.69166666666666,1.94497474683058));
#18668=CARTESIAN_POINT('Ctrl Pts',(0.,1.75,1.94497474683058));
#18669=CARTESIAN_POINT('Ctrl Pts',(-1.12293169364966,1.80833333333333,1.94497474683058));
#18670=CARTESIAN_POINT('Ctrl Pts',(-1.68439754047449,1.86666666666666,0.972487373415292));
#18671=CARTESIAN_POINT('Ctrl Pts',(-2.24586338729932,1.925,1.37519470428917E-16));
#18672=CARTESIAN_POINT('Ctrl Pts',(-1.68439754047449,1.98333333333333,-0.972487373415291));
#18673=CARTESIAN_POINT('Ctrl Pts',(-1.12293169364966,2.04166666666666,-1.94497474683058));
#18674=CARTESIAN_POINT('Ctrl Pts',(-2.38190709812851E-16,2.09999999999999,
-1.94497474683058));
#18675=CARTESIAN_POINT('Ctrl Pts',(1.12293169364966,2.15833333333333,-1.94497474683058));
#18676=CARTESIAN_POINT('Ctrl Pts',(1.68439754047449,2.21666666666666,-0.972487373415292));
#18677=CARTESIAN_POINT('Ctrl Pts',(2.24586338729932,2.275,-4.12558411286752E-16));
#18678=CARTESIAN_POINT('Ctrl Pts',(1.68439754047449,2.33333333333333,0.97248737341529));
#18679=CARTESIAN_POINT('Ctrl Pts',(1.12293169364966,2.39166666666666,1.94497474683058));
#18680=CARTESIAN_POINT('Ctrl Pts',(0.,2.44999999999999,1.94497474683058));
#18681=CARTESIAN_POINT('Ctrl Pts',(-1.12293169364966,2.50833333333333,1.94497474683058));
#18682=CARTESIAN_POINT('Ctrl Pts',(-1.68439754047449,2.56666666666666,0.972487373415292));
#18683=CARTESIAN_POINT('Ctrl Pts',(-2.24586338729932,2.62499999999999,1.37519470428917E-16));
#18684=CARTESIAN_POINT('Ctrl Pts',(-1.68439754047449,2.68333333333333,-0.972487373415291));
#18685=CARTESIAN_POINT('Ctrl Pts',(-1.12293169364966,2.74166666666666,-1.94497474683058));
#18686=CARTESIAN_POINT('Ctrl Pts',(-2.38190709812851E-16,2.79999999999999,
-1.94497474683058));
#18687=CARTESIAN_POINT('Ctrl Pts',(1.12293169364966,2.85833333333333,-1.94497474683058));
#18688=CARTESIAN_POINT('Ctrl Pts',(1.68439754047449,2.91666666666666,-0.972487373415292));
#18689=CARTESIAN_POINT('Ctrl Pts',(2.24586338729932,2.97499999999999,-4.12558411286752E-16));
#18690=CARTESIAN_POINT('Ctrl Pts',(1.68439754047449,3.03333333333333,0.97248737341529));
#18691=CARTESIAN_POINT('Ctrl Pts',(1.12293169364966,3.09166666666666,1.94497474683058));
#18692=CARTESIAN_POINT('Ctrl Pts',(0.,3.14999999999999,1.94497474683058));
#18693=CARTESIAN_POINT('Ctrl Pts',(-1.12293169364966,3.20833333333333,1.94497474683058));
#18694=CARTESIAN_POINT('Ctrl Pts',(-1.68439754047449,3.26666666666666,0.972487373415292));
#18695=CARTESIAN_POINT('Ctrl Pts',(-2.24586338729932,3.32499999999999,1.37519470428917E-16));
#18696=CARTESIAN_POINT('Ctrl Pts',(-1.68439754047449,3.38333333333333,-0.972487373415291));
#18697=CARTESIAN_POINT('Ctrl Pts',(-1.12293169364966,3.44166666666666,-1.94497474683058));
#18698=CARTESIAN_POINT('Ctrl Pts',(-2.38190709812851E-16,3.49999999999999,
-1.94497474683058));
#18699=CARTESIAN_POINT('Ctrl Pts',(1.12293169364966,3.55833333333333,-1.94497474683058));
#18700=CARTESIAN_POINT('Ctrl Pts',(1.68439754047449,3.61666666666666,-0.972487373415292));
#18701=CARTESIAN_POINT('Ctrl Pts',(2.24586338729932,3.67499999999999,-4.12558411286752E-16));
#18702=CARTESIAN_POINT('Ctrl Pts',(1.68439754047449,3.73333333333332,0.97248737341529));
#18703=CARTESIAN_POINT('Ctrl Pts',(1.12293169364966,3.79166666666666,1.94497474683058));
#18704=CARTESIAN_POINT('Ctrl Pts',(0.,3.84999999999999,1.94497474683058));
#18705=CARTESIAN_POINT('Ctrl Pts',(0.,-0.205025253169417,1.8));
#18706=CARTESIAN_POINT('Ctrl Pts',(-1.03923048454133,-0.146691919836083,
1.8));
#18707=CARTESIAN_POINT('Ctrl Pts',(-1.55884572681199,-0.0883585865027503,
0.9));
#18708=CARTESIAN_POINT('Ctrl Pts',(-2.07846096908265,-0.0300252531694171,
1.27269028646989E-16));
#18709=CARTESIAN_POINT('Ctrl Pts',(-1.55884572681199,0.0283080801639161,
-0.9));
#18710=CARTESIAN_POINT('Ctrl Pts',(-1.03923048454133,0.0866414134972494,
-1.8));
#18711=CARTESIAN_POINT('Ctrl Pts',(-2.20436423846524E-16,0.144974746830583,
-1.8));
#18712=CARTESIAN_POINT('Ctrl Pts',(1.03923048454133,0.203308080163916,-1.8));
#18713=CARTESIAN_POINT('Ctrl Pts',(1.55884572681199,0.261641413497249,-0.900000000000001));
#18714=CARTESIAN_POINT('Ctrl Pts',(2.07846096908265,0.319974746830582,-3.81807085940967E-16));
#18715=CARTESIAN_POINT('Ctrl Pts',(1.55884572681199,0.378308080163915,0.899999999999999));
#18716=CARTESIAN_POINT('Ctrl Pts',(1.03923048454133,0.436641413497249,1.8));
#18717=CARTESIAN_POINT('Ctrl Pts',(0.,0.494974746830582,1.8));
#18718=CARTESIAN_POINT('Ctrl Pts',(-1.03923048454133,0.553308080163915,
1.8));
#18719=CARTESIAN_POINT('Ctrl Pts',(-1.55884572681199,0.611641413497248,
0.9));
#18720=CARTESIAN_POINT('Ctrl Pts',(-2.07846096908265,0.669974746830582,
1.27269028646989E-16));
#18721=CARTESIAN_POINT('Ctrl Pts',(-1.55884572681199,0.728308080163915,
-0.9));
#18722=CARTESIAN_POINT('Ctrl Pts',(-1.03923048454133,0.786641413497248,
-1.8));
#18723=CARTESIAN_POINT('Ctrl Pts',(-2.20436423846524E-16,0.844974746830581,
-1.8));
#18724=CARTESIAN_POINT('Ctrl Pts',(1.03923048454133,0.903308080163914,-1.8));
#18725=CARTESIAN_POINT('Ctrl Pts',(1.55884572681199,0.961641413497248,-0.900000000000001));
#18726=CARTESIAN_POINT('Ctrl Pts',(2.07846096908265,1.01997474683058,-3.81807085940967E-16));
#18727=CARTESIAN_POINT('Ctrl Pts',(1.55884572681199,1.07830808016391,0.899999999999999));
#18728=CARTESIAN_POINT('Ctrl Pts',(1.03923048454133,1.13664141349725,1.8));
#18729=CARTESIAN_POINT('Ctrl Pts',(0.,1.19497474683058,1.8));
#18730=CARTESIAN_POINT('Ctrl Pts',(-1.03923048454133,1.25330808016391,1.8));
#18731=CARTESIAN_POINT('Ctrl Pts',(-1.55884572681199,1.31164141349725,0.9));
#18732=CARTESIAN_POINT('Ctrl Pts',(-2.07846096908265,1.36997474683058,1.27269028646989E-16));
#18733=CARTESIAN_POINT('Ctrl Pts',(-1.55884572681199,1.42830808016391,-0.9));
#18734=CARTESIAN_POINT('Ctrl Pts',(-1.03923048454133,1.48664141349725,-1.8));
#18735=CARTESIAN_POINT('Ctrl Pts',(-2.20436423846524E-16,1.54497474683058,
-1.8));
#18736=CARTESIAN_POINT('Ctrl Pts',(1.03923048454133,1.60330808016391,-1.8));
#18737=CARTESIAN_POINT('Ctrl Pts',(1.55884572681199,1.66164141349725,-0.900000000000001));
#18738=CARTESIAN_POINT('Ctrl Pts',(2.07846096908265,1.71997474683058,-3.81807085940967E-16));
#18739=CARTESIAN_POINT('Ctrl Pts',(1.55884572681199,1.77830808016391,0.899999999999999));
#18740=CARTESIAN_POINT('Ctrl Pts',(1.03923048454133,1.83664141349725,1.8));
#18741=CARTESIAN_POINT('Ctrl Pts',(0.,1.89497474683058,1.8));
#18742=CARTESIAN_POINT('Ctrl Pts',(-1.03923048454133,1.95330808016391,1.8));
#18743=CARTESIAN_POINT('Ctrl Pts',(-1.55884572681199,2.01164141349725,0.9));
#18744=CARTESIAN_POINT('Ctrl Pts',(-2.07846096908265,2.06997474683058,1.27269028646989E-16));
#18745=CARTESIAN_POINT('Ctrl Pts',(-1.55884572681199,2.12830808016391,-0.9));
#18746=CARTESIAN_POINT('Ctrl Pts',(-1.03923048454133,2.18664141349725,-1.8));
#18747=CARTESIAN_POINT('Ctrl Pts',(-2.20436423846524E-16,2.24497474683058,
-1.8));
#18748=CARTESIAN_POINT('Ctrl Pts',(1.03923048454133,2.30330808016391,-1.8));
#18749=CARTESIAN_POINT('Ctrl Pts',(1.55884572681199,2.36164141349724,-0.900000000000001));
#18750=CARTESIAN_POINT('Ctrl Pts',(2.07846096908265,2.41997474683058,-3.81807085940967E-16));
#18751=CARTESIAN_POINT('Ctrl Pts',(1.55884572681199,2.47830808016391,0.899999999999999));
#18752=CARTESIAN_POINT('Ctrl Pts',(1.03923048454133,2.53664141349724,1.8));
#18753=CARTESIAN_POINT('Ctrl Pts',(0.,2.59497474683058,1.8));
#18754=CARTESIAN_POINT('Ctrl Pts',(-1.03923048454133,2.65330808016391,1.8));
#18755=CARTESIAN_POINT('Ctrl Pts',(-1.55884572681199,2.71164141349724,0.9));
#18756=CARTESIAN_POINT('Ctrl Pts',(-2.07846096908265,2.76997474683058,1.27269028646989E-16));
#18757=CARTESIAN_POINT('Ctrl Pts',(-1.55884572681199,2.82830808016391,-0.9));
#18758=CARTESIAN_POINT('Ctrl Pts',(-1.03923048454133,2.88664141349724,-1.8));
#18759=CARTESIAN_POINT('Ctrl Pts',(-2.20436423846524E-16,2.94497474683058,
-1.8));
#18760=CARTESIAN_POINT('Ctrl Pts',(1.03923048454133,3.00330808016391,-1.8));
#18761=CARTESIAN_POINT('Ctrl Pts',(1.55884572681199,3.06164141349724,-0.900000000000001));
#18762=CARTESIAN_POINT('Ctrl Pts',(2.07846096908265,3.11997474683058,-3.81807085940967E-16));
#18763=CARTESIAN_POINT('Ctrl Pts',(1.55884572681199,3.17830808016391,0.899999999999999));
#18764=CARTESIAN_POINT('Ctrl Pts',(1.03923048454133,3.23664141349724,1.8));
#18765=CARTESIAN_POINT('Ctrl Pts',(0.,3.29497474683058,1.8));
#18766=CARTESIAN_POINT('Ctrl Pts',(-1.03923048454133,3.35330808016391,1.8));
#18767=CARTESIAN_POINT('Ctrl Pts',(-1.55884572681199,3.41164141349724,0.9));
#18768=CARTESIAN_POINT('Ctrl Pts',(-2.07846096908265,3.46997474683058,1.27269028646989E-16));
#18769=CARTESIAN_POINT('Ctrl Pts',(-1.55884572681199,3.52830808016391,-0.9));
#18770=CARTESIAN_POINT('Ctrl Pts',(-1.03923048454133,3.58664141349724,-1.8));
#18771=CARTESIAN_POINT('Ctrl Pts',(-2.20436423846524E-16,3.64497474683058,
-1.8));
#18772=CARTESIAN_POINT('Ctrl Pts',(1.03923048454133,3.70330808016391,-1.8));
#18773=CARTESIAN_POINT('Ctrl Pts',(1.55884572681199,3.76164141349724,-0.900000000000001));
#18774=CARTESIAN_POINT('Ctrl Pts',(2.07846096908265,3.81997474683058,-3.81807085940967E-16));
#18775=CARTESIAN_POINT('Ctrl Pts',(1.55884572681199,3.87830808016391,0.899999999999999));
#18776=CARTESIAN_POINT('Ctrl Pts',(1.03923048454133,3.93664141349724,1.8));
#18777=CARTESIAN_POINT('Ctrl Pts',(0.,3.99497474683058,1.8));
#18778=CARTESIAN_POINT('Ctrl Pts',(0.,0.,1.8));
#18779=CARTESIAN_POINT('Ctrl Pts',(-1.03923048454133,0.0583333333333332,
1.8));
#18780=CARTESIAN_POINT('Ctrl Pts',(-1.55884572681199,0.116666666666666,
0.9));
#18781=CARTESIAN_POINT('Ctrl Pts',(-2.07846096908265,0.175,1.27269028646989E-16));
#18782=CARTESIAN_POINT('Ctrl Pts',(-1.55884572681199,0.233333333333333,
-0.9));
#18783=CARTESIAN_POINT('Ctrl Pts',(-1.03923048454133,0.291666666666666,
-1.8));
#18784=CARTESIAN_POINT('Ctrl Pts',(-2.20436423846524E-16,0.349999999999999,
-1.8));
#18785=CARTESIAN_POINT('Ctrl Pts',(1.03923048454133,0.408333333333333,-1.8));
#18786=CARTESIAN_POINT('Ctrl Pts',(1.55884572681199,0.466666666666666,-0.900000000000001));
#18787=CARTESIAN_POINT('Ctrl Pts',(2.07846096908265,0.524999999999999,-3.81807085940967E-16));
#18788=CARTESIAN_POINT('Ctrl Pts',(1.55884572681199,0.583333333333332,0.899999999999999));
#18789=CARTESIAN_POINT('Ctrl Pts',(1.03923048454133,0.641666666666665,1.8));
#18790=CARTESIAN_POINT('Ctrl Pts',(0.,0.699999999999999,1.8));
#18791=CARTESIAN_POINT('Ctrl Pts',(-1.03923048454133,0.758333333333332,
1.8));
#18792=CARTESIAN_POINT('Ctrl Pts',(-1.55884572681199,0.816666666666665,
0.9));
#18793=CARTESIAN_POINT('Ctrl Pts',(-2.07846096908265,0.874999999999998,
1.27269028646989E-16));
#18794=CARTESIAN_POINT('Ctrl Pts',(-1.55884572681199,0.933333333333332,
-0.9));
#18795=CARTESIAN_POINT('Ctrl Pts',(-1.03923048454133,0.991666666666665,
-1.8));
#18796=CARTESIAN_POINT('Ctrl Pts',(-2.20436423846524E-16,1.05,-1.8));
#18797=CARTESIAN_POINT('Ctrl Pts',(1.03923048454133,1.10833333333333,-1.8));
#18798=CARTESIAN_POINT('Ctrl Pts',(1.55884572681199,1.16666666666666,-0.900000000000001));
#18799=CARTESIAN_POINT('Ctrl Pts',(2.07846096908265,1.225,-3.81807085940967E-16));
#18800=CARTESIAN_POINT('Ctrl Pts',(1.55884572681199,1.28333333333333,0.899999999999999));
#18801=CARTESIAN_POINT('Ctrl Pts',(1.03923048454133,1.34166666666666,1.8));
#18802=CARTESIAN_POINT('Ctrl Pts',(0.,1.4,1.8));
#18803=CARTESIAN_POINT('Ctrl Pts',(-1.03923048454133,1.45833333333333,1.8));
#18804=CARTESIAN_POINT('Ctrl Pts',(-1.55884572681199,1.51666666666666,0.9));
#18805=CARTESIAN_POINT('Ctrl Pts',(-2.07846096908265,1.575,1.27269028646989E-16));
#18806=CARTESIAN_POINT('Ctrl Pts',(-1.55884572681199,1.63333333333333,-0.9));
#18807=CARTESIAN_POINT('Ctrl Pts',(-1.03923048454133,1.69166666666666,-1.8));
#18808=CARTESIAN_POINT('Ctrl Pts',(-2.20436423846524E-16,1.75,-1.8));
#18809=CARTESIAN_POINT('Ctrl Pts',(1.03923048454133,1.80833333333333,-1.8));
#18810=CARTESIAN_POINT('Ctrl Pts',(1.55884572681199,1.86666666666666,-0.900000000000001));
#18811=CARTESIAN_POINT('Ctrl Pts',(2.07846096908265,1.925,-3.81807085940967E-16));
#18812=CARTESIAN_POINT('Ctrl Pts',(1.55884572681199,1.98333333333333,0.899999999999999));
#18813=CARTESIAN_POINT('Ctrl Pts',(1.03923048454133,2.04166666666666,1.8));
#18814=CARTESIAN_POINT('Ctrl Pts',(0.,2.1,1.8));
#18815=CARTESIAN_POINT('Ctrl Pts',(-1.03923048454133,2.15833333333333,1.8));
#18816=CARTESIAN_POINT('Ctrl Pts',(-1.55884572681199,2.21666666666666,0.9));
#18817=CARTESIAN_POINT('Ctrl Pts',(-2.07846096908265,2.275,1.27269028646989E-16));
#18818=CARTESIAN_POINT('Ctrl Pts',(-1.55884572681199,2.33333333333333,-0.9));
#18819=CARTESIAN_POINT('Ctrl Pts',(-1.03923048454133,2.39166666666666,-1.8));
#18820=CARTESIAN_POINT('Ctrl Pts',(-2.20436423846524E-16,2.45,-1.8));
#18821=CARTESIAN_POINT('Ctrl Pts',(1.03923048454133,2.50833333333333,-1.8));
#18822=CARTESIAN_POINT('Ctrl Pts',(1.55884572681199,2.56666666666666,-0.900000000000001));
#18823=CARTESIAN_POINT('Ctrl Pts',(2.07846096908265,2.62499999999999,-3.81807085940967E-16));
#18824=CARTESIAN_POINT('Ctrl Pts',(1.55884572681199,2.68333333333333,0.899999999999999));
#18825=CARTESIAN_POINT('Ctrl Pts',(1.03923048454133,2.74166666666666,1.8));
#18826=CARTESIAN_POINT('Ctrl Pts',(0.,2.79999999999999,1.8));
#18827=CARTESIAN_POINT('Ctrl Pts',(-1.03923048454133,2.85833333333333,1.8));
#18828=CARTESIAN_POINT('Ctrl Pts',(-1.55884572681199,2.91666666666666,0.9));
#18829=CARTESIAN_POINT('Ctrl Pts',(-2.07846096908265,2.97499999999999,1.27269028646989E-16));
#18830=CARTESIAN_POINT('Ctrl Pts',(-1.55884572681199,3.03333333333333,-0.9));
#18831=CARTESIAN_POINT('Ctrl Pts',(-1.03923048454133,3.09166666666666,-1.8));
#18832=CARTESIAN_POINT('Ctrl Pts',(-2.20436423846524E-16,3.14999999999999,
-1.8));
#18833=CARTESIAN_POINT('Ctrl Pts',(1.03923048454133,3.20833333333333,-1.8));
#18834=CARTESIAN_POINT('Ctrl Pts',(1.55884572681199,3.26666666666666,-0.900000000000001));
#18835=CARTESIAN_POINT('Ctrl Pts',(2.07846096908265,3.32499999999999,-3.81807085940967E-16));
#18836=CARTESIAN_POINT('Ctrl Pts',(1.55884572681199,3.38333333333333,0.899999999999999));
#18837=CARTESIAN_POINT('Ctrl Pts',(1.03923048454133,3.44166666666666,1.8));
#18838=CARTESIAN_POINT('Ctrl Pts',(0.,3.49999999999999,1.8));
#18839=CARTESIAN_POINT('Ctrl Pts',(-1.03923048454133,3.55833333333333,1.8));
#18840=CARTESIAN_POINT('Ctrl Pts',(-1.55884572681199,3.61666666666666,0.9));
#18841=CARTESIAN_POINT('Ctrl Pts',(-2.07846096908265,3.67499999999999,1.27269028646989E-16));
#18842=CARTESIAN_POINT('Ctrl Pts',(-1.55884572681199,3.73333333333333,-0.9));
#18843=CARTESIAN_POINT('Ctrl Pts',(-1.03923048454133,3.79166666666666,-1.8));
#18844=CARTESIAN_POINT('Ctrl Pts',(-2.20436423846524E-16,3.84999999999999,
-1.8));
#18845=CARTESIAN_POINT('Ctrl Pts',(1.03923048454133,3.90833333333333,-1.8));
#18846=CARTESIAN_POINT('Ctrl Pts',(1.55884572681199,3.96666666666666,-0.900000000000001));
#18847=CARTESIAN_POINT('Ctrl Pts',(2.07846096908265,4.02499999999999,-3.81807085940967E-16));
#18848=CARTESIAN_POINT('Ctrl Pts',(1.55884572681199,4.08333333333333,0.899999999999999));
#18849=CARTESIAN_POINT('Ctrl Pts',(1.03923048454133,4.14166666666666,1.8));
#18850=CARTESIAN_POINT('Ctrl Pts',(0.,4.19999999999999,1.8));
#18851=CARTESIAN_POINT('',(-2.63299061816681E-16,-0.349999999999999,2.15));
#18852=CARTESIAN_POINT('Origin',(0.,0.,2.15));
#18853=CARTESIAN_POINT('Ctrl Pts',(-2.63299061816681E-16,-0.349999999999999,
2.15));
#18854=CARTESIAN_POINT('Ctrl Pts',(-1.2413030787577,-0.291666666666666,
2.15));
#18855=CARTESIAN_POINT('Ctrl Pts',(-1.86195461813654,-0.233333333333333,
1.075));
#18856=CARTESIAN_POINT('Ctrl Pts',(-2.48260615751539,-0.175,-1.52015784217237E-16));
#18857=CARTESIAN_POINT('Ctrl Pts',(-1.86195461813654,-0.116666666666666,
-1.075));
#18858=CARTESIAN_POINT('Ctrl Pts',(-1.2413030787577,-0.0583333333333332,
-2.15));
#18859=CARTESIAN_POINT('Ctrl Pts',(0.,0.,-2.15));
#18860=CARTESIAN_POINT('Ctrl Pts',(1.24130307875769,0.0583333333333333,
-2.15));
#18861=CARTESIAN_POINT('Ctrl Pts',(1.86195461813654,0.116666666666666,-1.075));
#18862=CARTESIAN_POINT('Ctrl Pts',(2.48260615751539,0.175,-1.52015784217237E-16));
#18863=CARTESIAN_POINT('Ctrl Pts',(1.86195461813654,0.233333333333333,1.075));
#18864=CARTESIAN_POINT('Ctrl Pts',(1.2413030787577,0.291666666666666,2.15));
#18865=CARTESIAN_POINT('Ctrl Pts',(2.63299061816681E-16,0.349999999999999,
2.15));
#18866=CARTESIAN_POINT('Ctrl Pts',(2.63299061816681E-16,0.349999999999999,
2.15));
#18867=CARTESIAN_POINT('Ctrl Pts',(-1.24130307875769,0.408333333333333,
2.15));
#18868=CARTESIAN_POINT('Ctrl Pts',(-1.86195461813654,0.466666666666666,
1.075));
#18869=CARTESIAN_POINT('Ctrl Pts',(-2.48260615751539,0.524999999999999,
4.5604735265171E-16));
#18870=CARTESIAN_POINT('Ctrl Pts',(-1.86195461813654,0.583333333333332,
-1.075));
#18871=CARTESIAN_POINT('Ctrl Pts',(-1.2413030787577,0.641666666666665,-2.15));
#18872=CARTESIAN_POINT('Ctrl Pts',(-5.26598123633362E-16,0.699999999999999,
-2.15));
#18873=CARTESIAN_POINT('Ctrl Pts',(1.24130307875769,0.758333333333332,-2.15));
#18874=CARTESIAN_POINT('Ctrl Pts',(1.86195461813654,0.816666666666665,-1.075));
#18875=CARTESIAN_POINT('Ctrl Pts',(2.48260615751539,0.874999999999999,-7.60078921086183E-16));
#18876=CARTESIAN_POINT('Ctrl Pts',(1.86195461813654,0.933333333333332,1.075));
#18877=CARTESIAN_POINT('Ctrl Pts',(1.2413030787577,0.991666666666665,2.15));
#18878=CARTESIAN_POINT('Ctrl Pts',(7.89897185450043E-16,1.05,2.15));
#18879=CARTESIAN_POINT('Ctrl Pts',(-1.24130307875769,1.10833333333333,2.15));
#18880=CARTESIAN_POINT('Ctrl Pts',(-1.86195461813654,1.16666666666666,1.075));
#18881=CARTESIAN_POINT('Ctrl Pts',(-2.48260615751539,1.225,3.26910770324048E-15));
#18882=CARTESIAN_POINT('Ctrl Pts',(-1.86195461813654,1.28333333333333,-1.075));
#18883=CARTESIAN_POINT('Ctrl Pts',(-1.2413030787577,1.34166666666666,-2.15));
#18884=CARTESIAN_POINT('Ctrl Pts',(-1.05319624726672E-15,1.4,-2.15));
#18885=CARTESIAN_POINT('Ctrl Pts',(1.24130307875769,1.45833333333333,-2.15));
#18886=CARTESIAN_POINT('Ctrl Pts',(1.86195461813654,1.51666666666666,-1.075));
#18887=CARTESIAN_POINT('Ctrl Pts',(2.48260615751539,1.575,-1.36814205795513E-15));
#18888=CARTESIAN_POINT('Ctrl Pts',(1.86195461813654,1.63333333333333,1.075));
#18889=CARTESIAN_POINT('Ctrl Pts',(1.2413030787577,1.69166666666666,2.15));
#18890=CARTESIAN_POINT('Ctrl Pts',(1.3164953090834E-15,1.75,2.15));
#18891=CARTESIAN_POINT('Ctrl Pts',(-1.24130307875769,1.80833333333333,2.15));
#18892=CARTESIAN_POINT('Ctrl Pts',(-1.86195461813654,1.86666666666666,1.075));
#18893=CARTESIAN_POINT('Ctrl Pts',(-2.48260615751539,1.925,6.08216805382924E-15));
#18894=CARTESIAN_POINT('Ctrl Pts',(-1.86195461813654,1.98333333333333,-1.075));
#18895=CARTESIAN_POINT('Ctrl Pts',(-1.2413030787577,2.04166666666666,-2.15));
#18896=CARTESIAN_POINT('Ctrl Pts',(-5.39896157561062E-15,2.1,-2.15));
#18897=CARTESIAN_POINT('Ctrl Pts',(1.24130307875769,2.15833333333333,-2.15));
#18898=CARTESIAN_POINT('Ctrl Pts',(1.86195461813654,2.21666666666666,-1.075));
#18899=CARTESIAN_POINT('Ctrl Pts',(2.48260615751539,2.275,-6.38619962226372E-15));
#18900=CARTESIAN_POINT('Ctrl Pts',(1.86195461813655,2.33333333333333,1.07499999999999));
#18901=CARTESIAN_POINT('Ctrl Pts',(1.2413030787577,2.39166666666666,2.15));
#18902=CARTESIAN_POINT('Ctrl Pts',(1.84309343271677E-15,2.45,2.15));
#18903=CARTESIAN_POINT('Ctrl Pts',(-1.24130307875769,2.50833333333333,2.15));
#18904=CARTESIAN_POINT('Ctrl Pts',(-1.86195461813654,2.56666666666666,1.075));
#18905=CARTESIAN_POINT('Ctrl Pts',(-2.48260615751539,2.62499999999999,6.69023119069819E-15));
#18906=CARTESIAN_POINT('Ctrl Pts',(-1.86195461813655,2.68333333333333,-1.07499999999999));
#18907=CARTESIAN_POINT('Ctrl Pts',(-1.2413030787577,2.74166666666666,-2.14999999999999));
#18908=CARTESIAN_POINT('Ctrl Pts',(-2.10639249453345E-15,2.79999999999999,
-2.15));
#18909=CARTESIAN_POINT('Ctrl Pts',(1.24130307875769,2.85833333333333,-2.15));
#18910=CARTESIAN_POINT('Ctrl Pts',(1.86195461813654,2.91666666666666,-1.075));
#18911=CARTESIAN_POINT('Ctrl Pts',(2.48260615751539,2.97499999999999,-6.99426275913266E-15));
#18912=CARTESIAN_POINT('Ctrl Pts',(1.86195461813655,3.03333333333333,1.07499999999999));
#18913=CARTESIAN_POINT('Ctrl Pts',(1.2413030787577,3.09166666666666,2.14999999999999));
#18914=CARTESIAN_POINT('Ctrl Pts',(2.36969155635013E-15,3.14999999999999,
2.15));
#18915=CARTESIAN_POINT('Ctrl Pts',(-1.24130307875769,3.20833333333333,2.15));
#18916=CARTESIAN_POINT('Ctrl Pts',(-1.86195461813654,3.26666666666666,1.075));
#18917=CARTESIAN_POINT('Ctrl Pts',(-2.48260615751539,3.32499999999999,7.29829432756713E-15));
#18918=CARTESIAN_POINT('Ctrl Pts',(-1.86195461813655,3.38333333333333,-1.07499999999999));
#18919=CARTESIAN_POINT('Ctrl Pts',(-1.2413030787577,3.44166666666666,-2.14999999999999));
#18920=CARTESIAN_POINT('Ctrl Pts',(-1.02713250275879E-14,3.49999999999999,
-2.15));
#18921=CARTESIAN_POINT('Ctrl Pts',(1.24130307875769,3.55833333333333,-2.15));
#18922=CARTESIAN_POINT('Ctrl Pts',(1.86195461813654,3.61666666666666,-1.075));
#18923=CARTESIAN_POINT('Ctrl Pts',(2.48260615751539,3.67499999999999,-7.60232589600161E-15));
#18924=CARTESIAN_POINT('Ctrl Pts',(1.86195461813655,3.73333333333333,1.07499999999999));
#18925=CARTESIAN_POINT('Ctrl Pts',(1.2413030787577,3.79166666666666,2.14999999999999));
#18926=CARTESIAN_POINT('Ctrl Pts',(1.05346240894046E-14,3.84999999999999,
2.15));
#18927=CARTESIAN_POINT('Origin',(-1.80160437084306E-13,4.2,2.15));
#18928=CARTESIAN_POINT('Ctrl Pts',(0.,4.28626379701574E-17,2.5));
#18929=CARTESIAN_POINT('Ctrl Pts',(-1.44337567297406,0.0583333333333333,
2.5));
#18930=CARTESIAN_POINT('Ctrl Pts',(-2.1650635094611,0.116666666666666,1.25));
#18931=CARTESIAN_POINT('Ctrl Pts',(-2.88675134594813,0.175,1.76762539787484E-16));
#18932=CARTESIAN_POINT('Ctrl Pts',(-2.1650635094611,0.233333333333333,-1.25));
#18933=CARTESIAN_POINT('Ctrl Pts',(-1.44337567297407,0.291666666666666,
-2.5));
#18934=CARTESIAN_POINT('Ctrl Pts',(-3.06161699786838E-16,0.349999999999999,
-2.5));
#18935=CARTESIAN_POINT('Ctrl Pts',(1.44337567297406,0.408333333333333,-2.5));
#18936=CARTESIAN_POINT('Ctrl Pts',(2.1650635094611,0.466666666666666,-1.25));
#18937=CARTESIAN_POINT('Ctrl Pts',(2.88675134594813,0.524999999999999,-5.30287619362453E-16));
#18938=CARTESIAN_POINT('Ctrl Pts',(2.1650635094611,0.583333333333332,1.25));
#18939=CARTESIAN_POINT('Ctrl Pts',(1.44337567297407,0.641666666666665,2.5));
#18940=CARTESIAN_POINT('Ctrl Pts',(0.,0.699999999999999,2.5));
#18941=CARTESIAN_POINT('Ctrl Pts',(-1.44337567297406,0.758333333333332,
2.5));
#18942=CARTESIAN_POINT('Ctrl Pts',(-2.1650635094611,0.816666666666665,1.25));
#18943=CARTESIAN_POINT('Ctrl Pts',(-2.88675134594813,0.874999999999998,
1.76762539787484E-16));
#18944=CARTESIAN_POINT('Ctrl Pts',(-2.1650635094611,0.933333333333332,-1.25));
#18945=CARTESIAN_POINT('Ctrl Pts',(-1.44337567297407,0.991666666666665,
-2.5));
#18946=CARTESIAN_POINT('Ctrl Pts',(-3.06161699786838E-16,1.05,-2.5));
#18947=CARTESIAN_POINT('Ctrl Pts',(1.44337567297406,1.10833333333333,-2.5));
#18948=CARTESIAN_POINT('Ctrl Pts',(2.1650635094611,1.16666666666666,-1.25));
#18949=CARTESIAN_POINT('Ctrl Pts',(2.88675134594813,1.225,-5.30287619362453E-16));
#18950=CARTESIAN_POINT('Ctrl Pts',(2.1650635094611,1.28333333333333,1.25));
#18951=CARTESIAN_POINT('Ctrl Pts',(1.44337567297407,1.34166666666666,2.5));
#18952=CARTESIAN_POINT('Ctrl Pts',(0.,1.4,2.5));
#18953=CARTESIAN_POINT('Ctrl Pts',(-1.44337567297406,1.45833333333333,2.5));
#18954=CARTESIAN_POINT('Ctrl Pts',(-2.1650635094611,1.51666666666666,1.25));
#18955=CARTESIAN_POINT('Ctrl Pts',(-2.88675134594813,1.575,1.76762539787484E-16));
#18956=CARTESIAN_POINT('Ctrl Pts',(-2.1650635094611,1.63333333333333,-1.25));
#18957=CARTESIAN_POINT('Ctrl Pts',(-1.44337567297407,1.69166666666666,-2.5));
#18958=CARTESIAN_POINT('Ctrl Pts',(-3.06161699786838E-16,1.75,-2.5));
#18959=CARTESIAN_POINT('Ctrl Pts',(1.44337567297406,1.80833333333333,-2.5));
#18960=CARTESIAN_POINT('Ctrl Pts',(2.1650635094611,1.86666666666666,-1.25));
#18961=CARTESIAN_POINT('Ctrl Pts',(2.88675134594813,1.925,-5.30287619362453E-16));
#18962=CARTESIAN_POINT('Ctrl Pts',(2.1650635094611,1.98333333333333,1.25));
#18963=CARTESIAN_POINT('Ctrl Pts',(1.44337567297407,2.04166666666666,2.5));
#18964=CARTESIAN_POINT('Ctrl Pts',(0.,2.1,2.5));
#18965=CARTESIAN_POINT('Ctrl Pts',(-1.44337567297406,2.15833333333333,2.5));
#18966=CARTESIAN_POINT('Ctrl Pts',(-2.1650635094611,2.21666666666666,1.25));
#18967=CARTESIAN_POINT('Ctrl Pts',(-2.88675134594813,2.275,1.76762539787484E-16));
#18968=CARTESIAN_POINT('Ctrl Pts',(-2.1650635094611,2.33333333333333,-1.25));
#18969=CARTESIAN_POINT('Ctrl Pts',(-1.44337567297407,2.39166666666666,-2.5));
#18970=CARTESIAN_POINT('Ctrl Pts',(-3.06161699786838E-16,2.45,-2.5));
#18971=CARTESIAN_POINT('Ctrl Pts',(1.44337567297406,2.50833333333333,-2.5));
#18972=CARTESIAN_POINT('Ctrl Pts',(2.1650635094611,2.56666666666666,-1.25));
#18973=CARTESIAN_POINT('Ctrl Pts',(2.88675134594813,2.62499999999999,-5.30287619362453E-16));
#18974=CARTESIAN_POINT('Ctrl Pts',(2.1650635094611,2.68333333333333,1.25));
#18975=CARTESIAN_POINT('Ctrl Pts',(1.44337567297407,2.74166666666666,2.5));
#18976=CARTESIAN_POINT('Ctrl Pts',(0.,2.79999999999999,2.5));
#18977=CARTESIAN_POINT('Ctrl Pts',(-1.44337567297406,2.85833333333333,2.5));
#18978=CARTESIAN_POINT('Ctrl Pts',(-2.1650635094611,2.91666666666666,1.25));
#18979=CARTESIAN_POINT('Ctrl Pts',(-2.88675134594813,2.97499999999999,1.76762539787484E-16));
#18980=CARTESIAN_POINT('Ctrl Pts',(-2.1650635094611,3.03333333333333,-1.25));
#18981=CARTESIAN_POINT('Ctrl Pts',(-1.44337567297407,3.09166666666666,-2.5));
#18982=CARTESIAN_POINT('Ctrl Pts',(-3.06161699786838E-16,3.14999999999999,
-2.5));
#18983=CARTESIAN_POINT('Ctrl Pts',(1.44337567297406,3.20833333333333,-2.5));
#18984=CARTESIAN_POINT('Ctrl Pts',(2.1650635094611,3.26666666666666,-1.25));
#18985=CARTESIAN_POINT('Ctrl Pts',(2.88675134594813,3.32499999999999,-5.30287619362453E-16));
#18986=CARTESIAN_POINT('Ctrl Pts',(2.1650635094611,3.38333333333333,1.25));
#18987=CARTESIAN_POINT('Ctrl Pts',(1.44337567297407,3.44166666666666,2.5));
#18988=CARTESIAN_POINT('Ctrl Pts',(0.,3.49999999999999,2.5));
#18989=CARTESIAN_POINT('Ctrl Pts',(-1.44337567297406,3.55833333333333,2.5));
#18990=CARTESIAN_POINT('Ctrl Pts',(-2.1650635094611,3.61666666666666,1.25));
#18991=CARTESIAN_POINT('Ctrl Pts',(-2.88675134594813,3.67499999999999,1.76762539787484E-16));
#18992=CARTESIAN_POINT('Ctrl Pts',(-2.1650635094611,3.73333333333333,-1.25));
#18993=CARTESIAN_POINT('Ctrl Pts',(-1.44337567297407,3.79166666666666,-2.5));
#18994=CARTESIAN_POINT('Ctrl Pts',(-3.06161699786838E-16,3.84999999999999,
-2.5));
#18995=CARTESIAN_POINT('Ctrl Pts',(1.44337567297406,3.90833333333333,-2.5));
#18996=CARTESIAN_POINT('Ctrl Pts',(2.1650635094611,3.96666666666666,-1.25));
#18997=CARTESIAN_POINT('Ctrl Pts',(2.88675134594813,4.02499999999999,-5.30287619362453E-16));
#18998=CARTESIAN_POINT('Ctrl Pts',(2.1650635094611,4.08333333333333,1.25));
#18999=CARTESIAN_POINT('Ctrl Pts',(1.44337567297407,4.14166666666666,2.5));
#19000=CARTESIAN_POINT('Ctrl Pts',(0.,4.19999999999999,2.5));
#19001=CARTESIAN_POINT('Ctrl Pts',(0.,-0.205025253169417,2.5));
#19002=CARTESIAN_POINT('Ctrl Pts',(-1.44337567297406,-0.146691919836083,
2.5));
#19003=CARTESIAN_POINT('Ctrl Pts',(-2.1650635094611,-0.0883585865027503,
1.25));
#19004=CARTESIAN_POINT('Ctrl Pts',(-2.88675134594813,-0.0300252531694171,
1.76762539787484E-16));
#19005=CARTESIAN_POINT('Ctrl Pts',(-2.1650635094611,0.0283080801639162,
-1.25));
#19006=CARTESIAN_POINT('Ctrl Pts',(-1.44337567297407,0.0866414134972494,
-2.5));
#19007=CARTESIAN_POINT('Ctrl Pts',(-3.06161699786838E-16,0.144974746830583,
-2.5));
#19008=CARTESIAN_POINT('Ctrl Pts',(1.44337567297406,0.203308080163916,-2.5));
#19009=CARTESIAN_POINT('Ctrl Pts',(2.1650635094611,0.261641413497249,-1.25));
#19010=CARTESIAN_POINT('Ctrl Pts',(2.88675134594813,0.319974746830582,-5.30287619362453E-16));
#19011=CARTESIAN_POINT('Ctrl Pts',(2.1650635094611,0.378308080163915,1.25));
#19012=CARTESIAN_POINT('Ctrl Pts',(1.44337567297407,0.436641413497249,2.5));
#19013=CARTESIAN_POINT('Ctrl Pts',(0.,0.494974746830582,2.5));
#19014=CARTESIAN_POINT('Ctrl Pts',(-1.44337567297406,0.553308080163915,
2.5));
#19015=CARTESIAN_POINT('Ctrl Pts',(-2.1650635094611,0.611641413497248,1.25));
#19016=CARTESIAN_POINT('Ctrl Pts',(-2.88675134594813,0.669974746830582,
1.76762539787484E-16));
#19017=CARTESIAN_POINT('Ctrl Pts',(-2.1650635094611,0.728308080163915,-1.25));
#19018=CARTESIAN_POINT('Ctrl Pts',(-1.44337567297407,0.786641413497248,
-2.5));
#19019=CARTESIAN_POINT('Ctrl Pts',(-3.06161699786838E-16,0.844974746830581,
-2.5));
#19020=CARTESIAN_POINT('Ctrl Pts',(1.44337567297406,0.903308080163914,-2.5));
#19021=CARTESIAN_POINT('Ctrl Pts',(2.1650635094611,0.961641413497248,-1.25));
#19022=CARTESIAN_POINT('Ctrl Pts',(2.88675134594813,1.01997474683058,-5.30287619362453E-16));
#19023=CARTESIAN_POINT('Ctrl Pts',(2.1650635094611,1.07830808016391,1.25));
#19024=CARTESIAN_POINT('Ctrl Pts',(1.44337567297407,1.13664141349725,2.5));
#19025=CARTESIAN_POINT('Ctrl Pts',(0.,1.19497474683058,2.5));
#19026=CARTESIAN_POINT('Ctrl Pts',(-1.44337567297406,1.25330808016391,2.5));
#19027=CARTESIAN_POINT('Ctrl Pts',(-2.1650635094611,1.31164141349725,1.25));
#19028=CARTESIAN_POINT('Ctrl Pts',(-2.88675134594813,1.36997474683058,1.76762539787484E-16));
#19029=CARTESIAN_POINT('Ctrl Pts',(-2.1650635094611,1.42830808016391,-1.25));
#19030=CARTESIAN_POINT('Ctrl Pts',(-1.44337567297407,1.48664141349725,-2.5));
#19031=CARTESIAN_POINT('Ctrl Pts',(-3.06161699786838E-16,1.54497474683058,
-2.5));
#19032=CARTESIAN_POINT('Ctrl Pts',(1.44337567297406,1.60330808016391,-2.5));
#19033=CARTESIAN_POINT('Ctrl Pts',(2.1650635094611,1.66164141349725,-1.25));
#19034=CARTESIAN_POINT('Ctrl Pts',(2.88675134594813,1.71997474683058,-5.30287619362453E-16));
#19035=CARTESIAN_POINT('Ctrl Pts',(2.1650635094611,1.77830808016391,1.25));
#19036=CARTESIAN_POINT('Ctrl Pts',(1.44337567297407,1.83664141349725,2.5));
#19037=CARTESIAN_POINT('Ctrl Pts',(0.,1.89497474683058,2.5));
#19038=CARTESIAN_POINT('Ctrl Pts',(-1.44337567297406,1.95330808016391,2.5));
#19039=CARTESIAN_POINT('Ctrl Pts',(-2.1650635094611,2.01164141349725,1.25));
#19040=CARTESIAN_POINT('Ctrl Pts',(-2.88675134594813,2.06997474683058,1.76762539787484E-16));
#19041=CARTESIAN_POINT('Ctrl Pts',(-2.1650635094611,2.12830808016391,-1.25));
#19042=CARTESIAN_POINT('Ctrl Pts',(-1.44337567297407,2.18664141349725,-2.5));
#19043=CARTESIAN_POINT('Ctrl Pts',(-3.06161699786838E-16,2.24497474683058,
-2.5));
#19044=CARTESIAN_POINT('Ctrl Pts',(1.44337567297406,2.30330808016391,-2.5));
#19045=CARTESIAN_POINT('Ctrl Pts',(2.1650635094611,2.36164141349724,-1.25));
#19046=CARTESIAN_POINT('Ctrl Pts',(2.88675134594813,2.41997474683058,-5.30287619362453E-16));
#19047=CARTESIAN_POINT('Ctrl Pts',(2.1650635094611,2.47830808016391,1.25));
#19048=CARTESIAN_POINT('Ctrl Pts',(1.44337567297407,2.53664141349724,2.5));
#19049=CARTESIAN_POINT('Ctrl Pts',(0.,2.59497474683058,2.5));
#19050=CARTESIAN_POINT('Ctrl Pts',(-1.44337567297406,2.65330808016391,2.5));
#19051=CARTESIAN_POINT('Ctrl Pts',(-2.1650635094611,2.71164141349724,1.25));
#19052=CARTESIAN_POINT('Ctrl Pts',(-2.88675134594813,2.76997474683058,1.76762539787484E-16));
#19053=CARTESIAN_POINT('Ctrl Pts',(-2.1650635094611,2.82830808016391,-1.25));
#19054=CARTESIAN_POINT('Ctrl Pts',(-1.44337567297407,2.88664141349724,-2.5));
#19055=CARTESIAN_POINT('Ctrl Pts',(-3.06161699786838E-16,2.94497474683058,
-2.5));
#19056=CARTESIAN_POINT('Ctrl Pts',(1.44337567297406,3.00330808016391,-2.5));
#19057=CARTESIAN_POINT('Ctrl Pts',(2.1650635094611,3.06164141349724,-1.25));
#19058=CARTESIAN_POINT('Ctrl Pts',(2.88675134594813,3.11997474683058,-5.30287619362453E-16));
#19059=CARTESIAN_POINT('Ctrl Pts',(2.1650635094611,3.17830808016391,1.25));
#19060=CARTESIAN_POINT('Ctrl Pts',(1.44337567297407,3.23664141349724,2.5));
#19061=CARTESIAN_POINT('Ctrl Pts',(0.,3.29497474683058,2.5));
#19062=CARTESIAN_POINT('Ctrl Pts',(-1.44337567297406,3.35330808016391,2.5));
#19063=CARTESIAN_POINT('Ctrl Pts',(-2.1650635094611,3.41164141349724,1.25));
#19064=CARTESIAN_POINT('Ctrl Pts',(-2.88675134594813,3.46997474683058,1.76762539787484E-16));
#19065=CARTESIAN_POINT('Ctrl Pts',(-2.1650635094611,3.52830808016391,-1.25));
#19066=CARTESIAN_POINT('Ctrl Pts',(-1.44337567297407,3.58664141349724,-2.5));
#19067=CARTESIAN_POINT('Ctrl Pts',(-3.06161699786838E-16,3.64497474683058,
-2.5));
#19068=CARTESIAN_POINT('Ctrl Pts',(1.44337567297406,3.70330808016391,-2.5));
#19069=CARTESIAN_POINT('Ctrl Pts',(2.1650635094611,3.76164141349724,-1.25));
#19070=CARTESIAN_POINT('Ctrl Pts',(2.88675134594813,3.81997474683058,-5.30287619362453E-16));
#19071=CARTESIAN_POINT('Ctrl Pts',(2.1650635094611,3.87830808016391,1.25));
#19072=CARTESIAN_POINT('Ctrl Pts',(1.44337567297407,3.93664141349724,2.5));
#19073=CARTESIAN_POINT('Ctrl Pts',(0.,3.99497474683058,2.5));
#19074=CARTESIAN_POINT('Ctrl Pts',(0.,-0.35,2.35502525316942));
#19075=CARTESIAN_POINT('Ctrl Pts',(-1.35967446386573,-0.291666666666667,
2.35502525316942));
#19076=CARTESIAN_POINT('Ctrl Pts',(-2.03951169579859,-0.233333333333334,
1.17751262658471));
#19077=CARTESIAN_POINT('Ctrl Pts',(-2.71934892773146,-0.175,1.66512098005556E-16));
#19078=CARTESIAN_POINT('Ctrl Pts',(-2.03951169579859,-0.116666666666667,
-1.17751262658471));
#19079=CARTESIAN_POINT('Ctrl Pts',(-1.35967446386573,-0.0583333333333339,
-2.35502525316942));
#19080=CARTESIAN_POINT('Ctrl Pts',(-2.88407413820511E-16,-7.04731412115578E-16,
-2.35502525316942));
#19081=CARTESIAN_POINT('Ctrl Pts',(1.35967446386573,0.0583333333333326,
-2.35502525316942));
#19082=CARTESIAN_POINT('Ctrl Pts',(2.03951169579859,0.116666666666666,-1.17751262658471));
#19083=CARTESIAN_POINT('Ctrl Pts',(2.71934892773146,0.174999999999999,-4.99536294016668E-16));
#19084=CARTESIAN_POINT('Ctrl Pts',(2.03951169579859,0.233333333333332,1.17751262658471));
#19085=CARTESIAN_POINT('Ctrl Pts',(1.35967446386573,0.291666666666665,2.35502525316942));
#19086=CARTESIAN_POINT('Ctrl Pts',(0.,0.349999999999999,2.35502525316942));
#19087=CARTESIAN_POINT('Ctrl Pts',(-1.35967446386573,0.408333333333332,
2.35502525316942));
#19088=CARTESIAN_POINT('Ctrl Pts',(-2.03951169579859,0.466666666666665,
1.17751262658471));
#19089=CARTESIAN_POINT('Ctrl Pts',(-2.71934892773146,0.524999999999998,
1.66512098005556E-16));
#19090=CARTESIAN_POINT('Ctrl Pts',(-2.03951169579859,0.583333333333332,
-1.17751262658471));
#19091=CARTESIAN_POINT('Ctrl Pts',(-1.35967446386573,0.641666666666665,
-2.35502525316942));
#19092=CARTESIAN_POINT('Ctrl Pts',(-2.88407413820511E-16,0.699999999999998,
-2.35502525316942));
#19093=CARTESIAN_POINT('Ctrl Pts',(1.35967446386573,0.758333333333331,-2.35502525316942));
#19094=CARTESIAN_POINT('Ctrl Pts',(2.03951169579859,0.816666666666664,-1.17751262658471));
#19095=CARTESIAN_POINT('Ctrl Pts',(2.71934892773146,0.874999999999998,-4.99536294016668E-16));
#19096=CARTESIAN_POINT('Ctrl Pts',(2.03951169579859,0.933333333333331,1.17751262658471));
#19097=CARTESIAN_POINT('Ctrl Pts',(1.35967446386573,0.991666666666664,2.35502525316942));
#19098=CARTESIAN_POINT('Ctrl Pts',(0.,1.05,2.35502525316942));
#19099=CARTESIAN_POINT('Ctrl Pts',(-1.35967446386573,1.10833333333333,2.35502525316942));
#19100=CARTESIAN_POINT('Ctrl Pts',(-2.03951169579859,1.16666666666666,1.17751262658471));
#19101=CARTESIAN_POINT('Ctrl Pts',(-2.71934892773146,1.225,1.66512098005556E-16));
#19102=CARTESIAN_POINT('Ctrl Pts',(-2.03951169579859,1.28333333333333,-1.17751262658471));
#19103=CARTESIAN_POINT('Ctrl Pts',(-1.35967446386573,1.34166666666666,-2.35502525316942));
#19104=CARTESIAN_POINT('Ctrl Pts',(-2.88407413820511E-16,1.4,-2.35502525316942));
#19105=CARTESIAN_POINT('Ctrl Pts',(1.35967446386573,1.45833333333333,-2.35502525316942));
#19106=CARTESIAN_POINT('Ctrl Pts',(2.03951169579859,1.51666666666666,-1.17751262658471));
#19107=CARTESIAN_POINT('Ctrl Pts',(2.71934892773146,1.575,-4.99536294016668E-16));
#19108=CARTESIAN_POINT('Ctrl Pts',(2.03951169579859,1.63333333333333,1.17751262658471));
#19109=CARTESIAN_POINT('Ctrl Pts',(1.35967446386573,1.69166666666666,2.35502525316942));
#19110=CARTESIAN_POINT('Ctrl Pts',(0.,1.75,2.35502525316942));
#19111=CARTESIAN_POINT('Ctrl Pts',(-1.35967446386573,1.80833333333333,2.35502525316942));
#19112=CARTESIAN_POINT('Ctrl Pts',(-2.03951169579859,1.86666666666666,1.17751262658471));
#19113=CARTESIAN_POINT('Ctrl Pts',(-2.71934892773146,1.925,1.66512098005556E-16));
#19114=CARTESIAN_POINT('Ctrl Pts',(-2.03951169579859,1.98333333333333,-1.17751262658471));
#19115=CARTESIAN_POINT('Ctrl Pts',(-1.35967446386573,2.04166666666666,-2.35502525316942));
#19116=CARTESIAN_POINT('Ctrl Pts',(-2.88407413820511E-16,2.09999999999999,
-2.35502525316942));
#19117=CARTESIAN_POINT('Ctrl Pts',(1.35967446386573,2.15833333333333,-2.35502525316942));
#19118=CARTESIAN_POINT('Ctrl Pts',(2.03951169579859,2.21666666666666,-1.17751262658471));
#19119=CARTESIAN_POINT('Ctrl Pts',(2.71934892773146,2.275,-4.99536294016668E-16));
#19120=CARTESIAN_POINT('Ctrl Pts',(2.03951169579859,2.33333333333333,1.17751262658471));
#19121=CARTESIAN_POINT('Ctrl Pts',(1.35967446386573,2.39166666666666,2.35502525316942));
#19122=CARTESIAN_POINT('Ctrl Pts',(0.,2.44999999999999,2.35502525316942));
#19123=CARTESIAN_POINT('Ctrl Pts',(-1.35967446386573,2.50833333333333,2.35502525316942));
#19124=CARTESIAN_POINT('Ctrl Pts',(-2.03951169579859,2.56666666666666,1.17751262658471));
#19125=CARTESIAN_POINT('Ctrl Pts',(-2.71934892773146,2.62499999999999,1.66512098005556E-16));
#19126=CARTESIAN_POINT('Ctrl Pts',(-2.03951169579859,2.68333333333333,-1.17751262658471));
#19127=CARTESIAN_POINT('Ctrl Pts',(-1.35967446386573,2.74166666666666,-2.35502525316942));
#19128=CARTESIAN_POINT('Ctrl Pts',(-2.88407413820511E-16,2.79999999999999,
-2.35502525316942));
#19129=CARTESIAN_POINT('Ctrl Pts',(1.35967446386573,2.85833333333333,-2.35502525316942));
#19130=CARTESIAN_POINT('Ctrl Pts',(2.03951169579859,2.91666666666666,-1.17751262658471));
#19131=CARTESIAN_POINT('Ctrl Pts',(2.71934892773146,2.97499999999999,-4.99536294016668E-16));
#19132=CARTESIAN_POINT('Ctrl Pts',(2.03951169579859,3.03333333333333,1.17751262658471));
#19133=CARTESIAN_POINT('Ctrl Pts',(1.35967446386573,3.09166666666666,2.35502525316942));
#19134=CARTESIAN_POINT('Ctrl Pts',(0.,3.14999999999999,2.35502525316942));
#19135=CARTESIAN_POINT('Ctrl Pts',(-1.35967446386573,3.20833333333333,2.35502525316942));
#19136=CARTESIAN_POINT('Ctrl Pts',(-2.03951169579859,3.26666666666666,1.17751262658471));
#19137=CARTESIAN_POINT('Ctrl Pts',(-2.71934892773146,3.32499999999999,1.66512098005556E-16));
#19138=CARTESIAN_POINT('Ctrl Pts',(-2.03951169579859,3.38333333333333,-1.17751262658471));
#19139=CARTESIAN_POINT('Ctrl Pts',(-1.35967446386573,3.44166666666666,-2.35502525316942));
#19140=CARTESIAN_POINT('Ctrl Pts',(-2.88407413820511E-16,3.49999999999999,
-2.35502525316942));
#19141=CARTESIAN_POINT('Ctrl Pts',(1.35967446386573,3.55833333333333,-2.35502525316942));
#19142=CARTESIAN_POINT('Ctrl Pts',(2.03951169579859,3.61666666666666,-1.17751262658471));
#19143=CARTESIAN_POINT('Ctrl Pts',(2.71934892773146,3.67499999999999,-4.99536294016668E-16));
#19144=CARTESIAN_POINT('Ctrl Pts',(2.03951169579859,3.73333333333332,1.17751262658471));
#19145=CARTESIAN_POINT('Ctrl Pts',(1.35967446386573,3.79166666666666,2.35502525316942));
#19146=CARTESIAN_POINT('Ctrl Pts',(0.,3.84999999999999,2.35502525316942));
#19147=CARTESIAN_POINT('Ctrl Pts',(0.,-0.35,2.15));
#19148=CARTESIAN_POINT('Ctrl Pts',(-1.2413030787577,-0.291666666666667,
2.15));
#19149=CARTESIAN_POINT('Ctrl Pts',(-1.86195461813654,-0.233333333333334,
1.075));
#19150=CARTESIAN_POINT('Ctrl Pts',(-2.48260615751539,-0.175,1.52015784217237E-16));
#19151=CARTESIAN_POINT('Ctrl Pts',(-1.86195461813654,-0.116666666666667,
-1.075));
#19152=CARTESIAN_POINT('Ctrl Pts',(-1.2413030787577,-0.058333333333334,
-2.15));
#19153=CARTESIAN_POINT('Ctrl Pts',(-2.63299061816681E-16,-7.58941520739853E-16,
-2.15));
#19154=CARTESIAN_POINT('Ctrl Pts',(1.24130307875769,0.0583333333333325,
-2.15));
#19155=CARTESIAN_POINT('Ctrl Pts',(1.86195461813654,0.116666666666666,-1.075));
#19156=CARTESIAN_POINT('Ctrl Pts',(2.48260615751539,0.174999999999999,-4.5604735265171E-16));
#19157=CARTESIAN_POINT('Ctrl Pts',(1.86195461813654,0.233333333333332,1.075));
#19158=CARTESIAN_POINT('Ctrl Pts',(1.2413030787577,0.291666666666665,2.15));
#19159=CARTESIAN_POINT('Ctrl Pts',(0.,0.349999999999999,2.15));
#19160=CARTESIAN_POINT('Ctrl Pts',(-1.2413030787577,0.408333333333332,2.15));
#19161=CARTESIAN_POINT('Ctrl Pts',(-1.86195461813654,0.466666666666665,
1.075));
#19162=CARTESIAN_POINT('Ctrl Pts',(-2.48260615751539,0.524999999999998,
1.52015784217237E-16));
#19163=CARTESIAN_POINT('Ctrl Pts',(-1.86195461813654,0.583333333333331,
-1.075));
#19164=CARTESIAN_POINT('Ctrl Pts',(-1.2413030787577,0.641666666666665,-2.15));
#19165=CARTESIAN_POINT('Ctrl Pts',(-2.63299061816681E-16,0.699999999999998,
-2.15));
#19166=CARTESIAN_POINT('Ctrl Pts',(1.24130307875769,0.758333333333331,-2.15));
#19167=CARTESIAN_POINT('Ctrl Pts',(1.86195461813654,0.816666666666664,-1.075));
#19168=CARTESIAN_POINT('Ctrl Pts',(2.48260615751539,0.874999999999997,-4.5604735265171E-16));
#19169=CARTESIAN_POINT('Ctrl Pts',(1.86195461813654,0.933333333333331,1.075));
#19170=CARTESIAN_POINT('Ctrl Pts',(1.2413030787577,0.991666666666664,2.15));
#19171=CARTESIAN_POINT('Ctrl Pts',(0.,1.05,2.15));
#19172=CARTESIAN_POINT('Ctrl Pts',(-1.2413030787577,1.10833333333333,2.15));
#19173=CARTESIAN_POINT('Ctrl Pts',(-1.86195461813654,1.16666666666666,1.075));
#19174=CARTESIAN_POINT('Ctrl Pts',(-2.48260615751539,1.225,1.52015784217237E-16));
#19175=CARTESIAN_POINT('Ctrl Pts',(-1.86195461813654,1.28333333333333,-1.075));
#19176=CARTESIAN_POINT('Ctrl Pts',(-1.2413030787577,1.34166666666666,-2.15));
#19177=CARTESIAN_POINT('Ctrl Pts',(-2.63299061816681E-16,1.4,-2.15));
#19178=CARTESIAN_POINT('Ctrl Pts',(1.24130307875769,1.45833333333333,-2.15));
#19179=CARTESIAN_POINT('Ctrl Pts',(1.86195461813654,1.51666666666666,-1.075));
#19180=CARTESIAN_POINT('Ctrl Pts',(2.48260615751539,1.575,-4.5604735265171E-16));
#19181=CARTESIAN_POINT('Ctrl Pts',(1.86195461813654,1.63333333333333,1.075));
#19182=CARTESIAN_POINT('Ctrl Pts',(1.2413030787577,1.69166666666666,2.15));
#19183=CARTESIAN_POINT('Ctrl Pts',(0.,1.75,2.15));
#19184=CARTESIAN_POINT('Ctrl Pts',(-1.2413030787577,1.80833333333333,2.15));
#19185=CARTESIAN_POINT('Ctrl Pts',(-1.86195461813654,1.86666666666666,1.075));
#19186=CARTESIAN_POINT('Ctrl Pts',(-2.48260615751539,1.925,1.52015784217237E-16));
#19187=CARTESIAN_POINT('Ctrl Pts',(-1.86195461813654,1.98333333333333,-1.075));
#19188=CARTESIAN_POINT('Ctrl Pts',(-1.2413030787577,2.04166666666666,-2.15));
#19189=CARTESIAN_POINT('Ctrl Pts',(-2.63299061816681E-16,2.1,-2.15));
#19190=CARTESIAN_POINT('Ctrl Pts',(1.24130307875769,2.15833333333333,-2.15));
#19191=CARTESIAN_POINT('Ctrl Pts',(1.86195461813654,2.21666666666666,-1.075));
#19192=CARTESIAN_POINT('Ctrl Pts',(2.48260615751539,2.275,-4.5604735265171E-16));
#19193=CARTESIAN_POINT('Ctrl Pts',(1.86195461813654,2.33333333333333,1.075));
#19194=CARTESIAN_POINT('Ctrl Pts',(1.2413030787577,2.39166666666666,2.15));
#19195=CARTESIAN_POINT('Ctrl Pts',(0.,2.44999999999999,2.15));
#19196=CARTESIAN_POINT('Ctrl Pts',(-1.2413030787577,2.50833333333333,2.15));
#19197=CARTESIAN_POINT('Ctrl Pts',(-1.86195461813654,2.56666666666666,1.075));
#19198=CARTESIAN_POINT('Ctrl Pts',(-2.48260615751539,2.62499999999999,1.52015784217237E-16));
#19199=CARTESIAN_POINT('Ctrl Pts',(-1.86195461813654,2.68333333333333,-1.075));
#19200=CARTESIAN_POINT('Ctrl Pts',(-1.2413030787577,2.74166666666666,-2.15));
#19201=CARTESIAN_POINT('Ctrl Pts',(-2.63299061816681E-16,2.79999999999999,
-2.15));
#19202=CARTESIAN_POINT('Ctrl Pts',(1.24130307875769,2.85833333333333,-2.15));
#19203=CARTESIAN_POINT('Ctrl Pts',(1.86195461813654,2.91666666666666,-1.075));
#19204=CARTESIAN_POINT('Ctrl Pts',(2.48260615751539,2.97499999999999,-4.5604735265171E-16));
#19205=CARTESIAN_POINT('Ctrl Pts',(1.86195461813654,3.03333333333333,1.075));
#19206=CARTESIAN_POINT('Ctrl Pts',(1.2413030787577,3.09166666666666,2.15));
#19207=CARTESIAN_POINT('Ctrl Pts',(0.,3.14999999999999,2.15));
#19208=CARTESIAN_POINT('Ctrl Pts',(-1.2413030787577,3.20833333333333,2.15));
#19209=CARTESIAN_POINT('Ctrl Pts',(-1.86195461813654,3.26666666666666,1.075));
#19210=CARTESIAN_POINT('Ctrl Pts',(-2.48260615751539,3.32499999999999,1.52015784217237E-16));
#19211=CARTESIAN_POINT('Ctrl Pts',(-1.86195461813654,3.38333333333333,-1.075));
#19212=CARTESIAN_POINT('Ctrl Pts',(-1.2413030787577,3.44166666666666,-2.15));
#19213=CARTESIAN_POINT('Ctrl Pts',(-2.63299061816681E-16,3.49999999999999,
-2.15));
#19214=CARTESIAN_POINT('Ctrl Pts',(1.24130307875769,3.55833333333333,-2.15));
#19215=CARTESIAN_POINT('Ctrl Pts',(1.86195461813654,3.61666666666666,-1.075));
#19216=CARTESIAN_POINT('Ctrl Pts',(2.48260615751539,3.67499999999999,-4.5604735265171E-16));
#19217=CARTESIAN_POINT('Ctrl Pts',(1.86195461813654,3.73333333333333,1.075));
#19218=CARTESIAN_POINT('Ctrl Pts',(1.2413030787577,3.79166666666666,2.15));
#19219=CARTESIAN_POINT('Ctrl Pts',(0.,3.84999999999999,2.15));
#19220=CARTESIAN_POINT('',(0.,4.28626379701574E-17,2.5));
#19221=CARTESIAN_POINT('Origin',(0.,0.,2.15));
#19222=CARTESIAN_POINT('',(-1.02907469966573E-13,4.2,2.5));
#19223=CARTESIAN_POINT('Ctrl Pts',(0.,4.28626379701574E-17,2.5));
#19224=CARTESIAN_POINT('Ctrl Pts',(-1.44337567297406,0.0583333333333333,
2.5));
#19225=CARTESIAN_POINT('Ctrl Pts',(-2.1650635094611,0.116666666666666,1.25));
#19226=CARTESIAN_POINT('Ctrl Pts',(-2.88675134594813,0.175,1.76762539787484E-16));
#19227=CARTESIAN_POINT('Ctrl Pts',(-2.1650635094611,0.233333333333333,-1.25));
#19228=CARTESIAN_POINT('Ctrl Pts',(-1.44337567297407,0.291666666666666,
-2.5));
#19229=CARTESIAN_POINT('Ctrl Pts',(-3.06161699786838E-16,0.349999999999999,
-2.5));
#19230=CARTESIAN_POINT('Ctrl Pts',(1.44337567297406,0.408333333333333,-2.5));
#19231=CARTESIAN_POINT('Ctrl Pts',(2.1650635094611,0.466666666666666,-1.25));
#19232=CARTESIAN_POINT('Ctrl Pts',(2.88675134594813,0.524999999999999,-5.30287619362453E-16));
#19233=CARTESIAN_POINT('Ctrl Pts',(2.1650635094611,0.583333333333332,1.25));
#19234=CARTESIAN_POINT('Ctrl Pts',(1.44337567297407,0.641666666666665,2.5));
#19235=CARTESIAN_POINT('Ctrl Pts',(6.12323399573677E-16,0.699999999999999,
2.5));
#19236=CARTESIAN_POINT('Ctrl Pts',(-1.44337567297406,0.758333333333332,
2.5));
#19237=CARTESIAN_POINT('Ctrl Pts',(-2.1650635094611,0.816666666666665,1.25));
#19238=CARTESIAN_POINT('Ctrl Pts',(-2.88675134594813,0.874999999999998,
3.44776294744884E-15));
#19239=CARTESIAN_POINT('Ctrl Pts',(-2.1650635094611,0.933333333333332,-1.25));
#19240=CARTESIAN_POINT('Ctrl Pts',(-1.44337567297407,0.991666666666665,
-2.5));
#19241=CARTESIAN_POINT('Ctrl Pts',(-9.18485099360515E-16,1.05,-2.5));
#19242=CARTESIAN_POINT('Ctrl Pts',(1.44337567297406,1.10833333333333,-2.5));
#19243=CARTESIAN_POINT('Ctrl Pts',(2.16506350946109,1.16666666666666,-1.25));
#19244=CARTESIAN_POINT('Ctrl Pts',(2.88675134594813,1.225,-1.23733777851239E-15));
#19245=CARTESIAN_POINT('Ctrl Pts',(2.1650635094611,1.28333333333333,1.25));
#19246=CARTESIAN_POINT('Ctrl Pts',(1.44337567297407,1.34166666666666,2.5));
#19247=CARTESIAN_POINT('Ctrl Pts',(1.22464679914735E-15,1.4,2.5));
#19248=CARTESIAN_POINT('Ctrl Pts',(-1.44337567297406,1.45833333333333,2.5));
#19249=CARTESIAN_POINT('Ctrl Pts',(-2.16506350946109,1.51666666666666,1.25));
#19250=CARTESIAN_POINT('Ctrl Pts',(-2.88675134594813,1.575,6.7187633551102E-15));
#19251=CARTESIAN_POINT('Ctrl Pts',(-2.1650635094611,1.63333333333333,-1.25));
#19252=CARTESIAN_POINT('Ctrl Pts',(-1.44337567297407,1.69166666666666,-2.5));
#19253=CARTESIAN_POINT('Ctrl Pts',(-5.97170059743482E-15,1.75,-2.5));
#19254=CARTESIAN_POINT('Ctrl Pts',(1.44337567297406,1.80833333333333,-2.5));
#19255=CARTESIAN_POINT('Ctrl Pts',(2.16506350946109,1.86666666666666,-1.25));
#19256=CARTESIAN_POINT('Ctrl Pts',(2.88675134594813,1.925,-7.07228843468517E-15));
#19257=CARTESIAN_POINT('Ctrl Pts',(2.1650635094611,1.98333333333333,1.24999999999999));
#19258=CARTESIAN_POINT('Ctrl Pts',(1.44337567297407,2.04166666666666,2.49999999999999));
#19259=CARTESIAN_POINT('Ctrl Pts',(1.83697019872103E-15,2.1,2.5));
#19260=CARTESIAN_POINT('Ctrl Pts',(-1.44337567297406,2.15833333333333,2.5));
#19261=CARTESIAN_POINT('Ctrl Pts',(-2.16506350946109,2.21666666666666,1.25));
#19262=CARTESIAN_POINT('Ctrl Pts',(-2.88675134594813,2.275,7.42581351426014E-15));
#19263=CARTESIAN_POINT('Ctrl Pts',(-2.1650635094611,2.33333333333333,-1.24999999999999));
#19264=CARTESIAN_POINT('Ctrl Pts',(-1.44337567297407,2.39166666666666,-2.49999999999999));
#19265=CARTESIAN_POINT('Ctrl Pts',(-2.14313189850787E-15,2.45,-2.5));
#19266=CARTESIAN_POINT('Ctrl Pts',(1.44337567297406,2.50833333333333,-2.5));
#19267=CARTESIAN_POINT('Ctrl Pts',(2.16506350946109,2.56666666666666,-1.25));
#19268=CARTESIAN_POINT('Ctrl Pts',(2.88675134594813,2.625,-7.7793385938351E-15));
#19269=CARTESIAN_POINT('Ctrl Pts',(2.1650635094611,2.68333333333333,1.24999999999999));
#19270=CARTESIAN_POINT('Ctrl Pts',(1.44337567297407,2.74166666666666,2.49999999999999));
#19271=CARTESIAN_POINT('Ctrl Pts',(2.44929359829471E-15,2.79999999999999,
2.5));
#19272=CARTESIAN_POINT('Ctrl Pts',(-1.44337567297406,2.85833333333333,2.5));
#19273=CARTESIAN_POINT('Ctrl Pts',(-2.16506350946109,2.91666666666666,1.25));
#19274=CARTESIAN_POINT('Ctrl Pts',(-2.88675134594813,2.97499999999999,8.13286367341007E-15));
#19275=CARTESIAN_POINT('Ctrl Pts',(-2.1650635094611,3.03333333333333,-1.24999999999999));
#19276=CARTESIAN_POINT('Ctrl Pts',(-1.44337567297407,3.09166666666666,-2.49999999999999));
#19277=CARTESIAN_POINT('Ctrl Pts',(-1.16372394950828E-14,3.14999999999999,
-2.5));
#19278=CARTESIAN_POINT('Ctrl Pts',(1.44337567297406,3.20833333333333,-2.5));
#19279=CARTESIAN_POINT('Ctrl Pts',(2.16506350946109,3.26666666666666,-1.25000000000001));
#19280=CARTESIAN_POINT('Ctrl Pts',(2.88675134594813,3.32499999999999,-8.48638875298504E-15));
#19281=CARTESIAN_POINT('Ctrl Pts',(2.1650635094611,3.38333333333333,1.24999999999999));
#19282=CARTESIAN_POINT('Ctrl Pts',(1.44337567297407,3.44166666666666,2.49999999999999));
#19283=CARTESIAN_POINT('Ctrl Pts',(1.19434011948696E-14,3.49999999999999,
2.5));
#19284=CARTESIAN_POINT('Ctrl Pts',(-1.44337567297406,3.55833333333333,2.5));
#19285=CARTESIAN_POINT('Ctrl Pts',(-2.16506350946109,3.61666666666666,1.25000000000001));
#19286=CARTESIAN_POINT('Ctrl Pts',(-2.88675134594813,3.67499999999999,1.90957148266057E-14));
#19287=CARTESIAN_POINT('Ctrl Pts',(-2.1650635094611,3.73333333333333,-1.24999999999999));
#19288=CARTESIAN_POINT('Ctrl Pts',(-1.44337567297407,3.79166666666666,-2.5));
#19289=CARTESIAN_POINT('Ctrl Pts',(-1.22495628946565E-14,3.84999999999999,
-2.5));
#19290=CARTESIAN_POINT('Ctrl Pts',(1.44337567297406,3.90833333333333,-2.5));
#19291=CARTESIAN_POINT('Ctrl Pts',(2.16506350946109,3.96666666666666,-1.25000000000001));
#19292=CARTESIAN_POINT('Ctrl Pts',(2.88675134594813,4.02499999999999,-9.19343891213498E-15));
#19293=CARTESIAN_POINT('Ctrl Pts',(2.16506350946111,4.08333333333333,1.24999999999998));
#19294=CARTESIAN_POINT('Ctrl Pts',(1.44337567297408,4.14166666666666,2.49999999999999));
#19295=CARTESIAN_POINT('Ctrl Pts',(-1.02907469966573E-13,4.2,2.5));
#19296=CARTESIAN_POINT('Origin',(-1.80160437084306E-13,4.2,2.15));
#19297=CARTESIAN_POINT('Ctrl Pts',(0.,0.35,2.15));
#19298=CARTESIAN_POINT('Ctrl Pts',(-1.2413030787577,0.408333333333333,2.15));
#19299=CARTESIAN_POINT('Ctrl Pts',(-1.86195461813654,0.466666666666667,
1.075));
#19300=CARTESIAN_POINT('Ctrl Pts',(-2.48260615751539,0.525,1.52015784217237E-16));
#19301=CARTESIAN_POINT('Ctrl Pts',(-1.86195461813654,0.583333333333333,
-1.075));
#19302=CARTESIAN_POINT('Ctrl Pts',(-1.2413030787577,0.641666666666666,-2.15));
#19303=CARTESIAN_POINT('Ctrl Pts',(-2.63299061816681E-16,0.699999999999999,
-2.15));
#19304=CARTESIAN_POINT('Ctrl Pts',(1.24130307875769,0.758333333333333,-2.15));
#19305=CARTESIAN_POINT('Ctrl Pts',(1.86195461813654,0.816666666666666,-1.075));
#19306=CARTESIAN_POINT('Ctrl Pts',(2.48260615751539,0.874999999999999,-4.5604735265171E-16));
#19307=CARTESIAN_POINT('Ctrl Pts',(1.86195461813654,0.933333333333332,1.075));
#19308=CARTESIAN_POINT('Ctrl Pts',(1.2413030787577,0.991666666666666,2.15));
#19309=CARTESIAN_POINT('Ctrl Pts',(0.,1.05,2.15));
#19310=CARTESIAN_POINT('Ctrl Pts',(-1.2413030787577,1.10833333333333,2.15));
#19311=CARTESIAN_POINT('Ctrl Pts',(-1.86195461813654,1.16666666666667,1.075));
#19312=CARTESIAN_POINT('Ctrl Pts',(-2.48260615751539,1.225,1.52015784217237E-16));
#19313=CARTESIAN_POINT('Ctrl Pts',(-1.86195461813654,1.28333333333333,-1.075));
#19314=CARTESIAN_POINT('Ctrl Pts',(-1.2413030787577,1.34166666666666,-2.15));
#19315=CARTESIAN_POINT('Ctrl Pts',(-2.63299061816681E-16,1.4,-2.15));
#19316=CARTESIAN_POINT('Ctrl Pts',(1.24130307875769,1.45833333333333,-2.15));
#19317=CARTESIAN_POINT('Ctrl Pts',(1.86195461813654,1.51666666666666,-1.075));
#19318=CARTESIAN_POINT('Ctrl Pts',(2.48260615751539,1.575,-4.5604735265171E-16));
#19319=CARTESIAN_POINT('Ctrl Pts',(1.86195461813654,1.63333333333333,1.075));
#19320=CARTESIAN_POINT('Ctrl Pts',(1.2413030787577,1.69166666666666,2.15));
#19321=CARTESIAN_POINT('Ctrl Pts',(0.,1.75,2.15));
#19322=CARTESIAN_POINT('Ctrl Pts',(-1.2413030787577,1.80833333333333,2.15));
#19323=CARTESIAN_POINT('Ctrl Pts',(-1.86195461813654,1.86666666666666,1.075));
#19324=CARTESIAN_POINT('Ctrl Pts',(-2.48260615751539,1.925,1.52015784217237E-16));
#19325=CARTESIAN_POINT('Ctrl Pts',(-1.86195461813654,1.98333333333333,-1.075));
#19326=CARTESIAN_POINT('Ctrl Pts',(-1.2413030787577,2.04166666666666,-2.15));
#19327=CARTESIAN_POINT('Ctrl Pts',(-2.63299061816681E-16,2.1,-2.15));
#19328=CARTESIAN_POINT('Ctrl Pts',(1.24130307875769,2.15833333333333,-2.15));
#19329=CARTESIAN_POINT('Ctrl Pts',(1.86195461813654,2.21666666666666,-1.075));
#19330=CARTESIAN_POINT('Ctrl Pts',(2.48260615751539,2.275,-4.5604735265171E-16));
#19331=CARTESIAN_POINT('Ctrl Pts',(1.86195461813654,2.33333333333333,1.075));
#19332=CARTESIAN_POINT('Ctrl Pts',(1.2413030787577,2.39166666666666,2.15));
#19333=CARTESIAN_POINT('Ctrl Pts',(0.,2.45,2.15));
#19334=CARTESIAN_POINT('Ctrl Pts',(-1.2413030787577,2.50833333333333,2.15));
#19335=CARTESIAN_POINT('Ctrl Pts',(-1.86195461813654,2.56666666666666,1.075));
#19336=CARTESIAN_POINT('Ctrl Pts',(-2.48260615751539,2.625,1.52015784217237E-16));
#19337=CARTESIAN_POINT('Ctrl Pts',(-1.86195461813654,2.68333333333333,-1.075));
#19338=CARTESIAN_POINT('Ctrl Pts',(-1.2413030787577,2.74166666666666,-2.15));
#19339=CARTESIAN_POINT('Ctrl Pts',(-2.63299061816681E-16,2.8,-2.15));
#19340=CARTESIAN_POINT('Ctrl Pts',(1.24130307875769,2.85833333333333,-2.15));
#19341=CARTESIAN_POINT('Ctrl Pts',(1.86195461813654,2.91666666666666,-1.075));
#19342=CARTESIAN_POINT('Ctrl Pts',(2.48260615751539,2.97499999999999,-4.5604735265171E-16));
#19343=CARTESIAN_POINT('Ctrl Pts',(1.86195461813654,3.03333333333333,1.075));
#19344=CARTESIAN_POINT('Ctrl Pts',(1.2413030787577,3.09166666666666,2.15));
#19345=CARTESIAN_POINT('Ctrl Pts',(0.,3.15,2.15));
#19346=CARTESIAN_POINT('Ctrl Pts',(-1.2413030787577,3.20833333333333,2.15));
#19347=CARTESIAN_POINT('Ctrl Pts',(-1.86195461813654,3.26666666666666,1.075));
#19348=CARTESIAN_POINT('Ctrl Pts',(-2.48260615751539,3.32499999999999,1.52015784217237E-16));
#19349=CARTESIAN_POINT('Ctrl Pts',(-1.86195461813654,3.38333333333333,-1.075));
#19350=CARTESIAN_POINT('Ctrl Pts',(-1.2413030787577,3.44166666666666,-2.15));
#19351=CARTESIAN_POINT('Ctrl Pts',(-2.63299061816681E-16,3.49999999999999,
-2.15));
#19352=CARTESIAN_POINT('Ctrl Pts',(1.24130307875769,3.55833333333333,-2.15));
#19353=CARTESIAN_POINT('Ctrl Pts',(1.86195461813654,3.61666666666666,-1.075));
#19354=CARTESIAN_POINT('Ctrl Pts',(2.48260615751539,3.67499999999999,-4.5604735265171E-16));
#19355=CARTESIAN_POINT('Ctrl Pts',(1.86195461813654,3.73333333333333,1.075));
#19356=CARTESIAN_POINT('Ctrl Pts',(1.2413030787577,3.79166666666666,2.15));
#19357=CARTESIAN_POINT('Ctrl Pts',(0.,3.84999999999999,2.15));
#19358=CARTESIAN_POINT('Ctrl Pts',(-1.2413030787577,3.90833333333333,2.15));
#19359=CARTESIAN_POINT('Ctrl Pts',(-1.86195461813654,3.96666666666666,1.075));
#19360=CARTESIAN_POINT('Ctrl Pts',(-2.48260615751539,4.02499999999999,1.52015784217237E-16));
#19361=CARTESIAN_POINT('Ctrl Pts',(-1.86195461813654,4.08333333333333,-1.075));
#19362=CARTESIAN_POINT('Ctrl Pts',(-1.2413030787577,4.14166666666666,-2.15));
#19363=CARTESIAN_POINT('Ctrl Pts',(-2.63299061816681E-16,4.19999999999999,
-2.15));
#19364=CARTESIAN_POINT('Ctrl Pts',(1.24130307875769,4.25833333333333,-2.15));
#19365=CARTESIAN_POINT('Ctrl Pts',(1.86195461813654,4.31666666666666,-1.075));
#19366=CARTESIAN_POINT('Ctrl Pts',(2.48260615751539,4.37499999999999,-4.5604735265171E-16));
#19367=CARTESIAN_POINT('Ctrl Pts',(1.86195461813654,4.43333333333333,1.075));
#19368=CARTESIAN_POINT('Ctrl Pts',(1.2413030787577,4.49166666666666,2.15));
#19369=CARTESIAN_POINT('Ctrl Pts',(0.,4.54999999999999,2.15));
#19370=CARTESIAN_POINT('Ctrl Pts',(0.,0.35,2.35502525316942));
#19371=CARTESIAN_POINT('Ctrl Pts',(-1.35967446386573,0.408333333333333,
2.35502525316942));
#19372=CARTESIAN_POINT('Ctrl Pts',(-2.03951169579859,0.466666666666666,
1.17751262658471));
#19373=CARTESIAN_POINT('Ctrl Pts',(-2.71934892773146,0.525,1.66512098005556E-16));
#19374=CARTESIAN_POINT('Ctrl Pts',(-2.03951169579859,0.583333333333333,
-1.17751262658471));
#19375=CARTESIAN_POINT('Ctrl Pts',(-1.35967446386573,0.641666666666666,
-2.35502525316942));
#19376=CARTESIAN_POINT('Ctrl Pts',(-2.88407413820511E-16,0.699999999999999,
-2.35502525316942));
#19377=CARTESIAN_POINT('Ctrl Pts',(1.35967446386573,0.758333333333333,-2.35502525316942));
#19378=CARTESIAN_POINT('Ctrl Pts',(2.03951169579859,0.816666666666666,-1.17751262658471));
#19379=CARTESIAN_POINT('Ctrl Pts',(2.71934892773146,0.874999999999999,-4.99536294016668E-16));
#19380=CARTESIAN_POINT('Ctrl Pts',(2.03951169579859,0.933333333333332,1.17751262658471));
#19381=CARTESIAN_POINT('Ctrl Pts',(1.35967446386573,0.991666666666665,2.35502525316942));
#19382=CARTESIAN_POINT('Ctrl Pts',(0.,1.05,2.35502525316942));
#19383=CARTESIAN_POINT('Ctrl Pts',(-1.35967446386573,1.10833333333333,2.35502525316942));
#19384=CARTESIAN_POINT('Ctrl Pts',(-2.03951169579859,1.16666666666666,1.17751262658471));
#19385=CARTESIAN_POINT('Ctrl Pts',(-2.71934892773146,1.225,1.66512098005556E-16));
#19386=CARTESIAN_POINT('Ctrl Pts',(-2.03951169579859,1.28333333333333,-1.17751262658471));
#19387=CARTESIAN_POINT('Ctrl Pts',(-1.35967446386573,1.34166666666667,-2.35502525316942));
#19388=CARTESIAN_POINT('Ctrl Pts',(-2.88407413820511E-16,1.4,-2.35502525316942));
#19389=CARTESIAN_POINT('Ctrl Pts',(1.35967446386573,1.45833333333333,-2.35502525316942));
#19390=CARTESIAN_POINT('Ctrl Pts',(2.03951169579859,1.51666666666666,-1.17751262658471));
#19391=CARTESIAN_POINT('Ctrl Pts',(2.71934892773146,1.575,-4.99536294016668E-16));
#19392=CARTESIAN_POINT('Ctrl Pts',(2.03951169579859,1.63333333333333,1.17751262658471));
#19393=CARTESIAN_POINT('Ctrl Pts',(1.35967446386573,1.69166666666666,2.35502525316942));
#19394=CARTESIAN_POINT('Ctrl Pts',(0.,1.75,2.35502525316942));
#19395=CARTESIAN_POINT('Ctrl Pts',(-1.35967446386573,1.80833333333333,2.35502525316942));
#19396=CARTESIAN_POINT('Ctrl Pts',(-2.03951169579859,1.86666666666666,1.17751262658471));
#19397=CARTESIAN_POINT('Ctrl Pts',(-2.71934892773146,1.925,1.66512098005556E-16));
#19398=CARTESIAN_POINT('Ctrl Pts',(-2.03951169579859,1.98333333333333,-1.17751262658471));
#19399=CARTESIAN_POINT('Ctrl Pts',(-1.35967446386573,2.04166666666666,-2.35502525316942));
#19400=CARTESIAN_POINT('Ctrl Pts',(-2.88407413820511E-16,2.1,-2.35502525316942));
#19401=CARTESIAN_POINT('Ctrl Pts',(1.35967446386573,2.15833333333333,-2.35502525316942));
#19402=CARTESIAN_POINT('Ctrl Pts',(2.03951169579859,2.21666666666666,-1.17751262658471));
#19403=CARTESIAN_POINT('Ctrl Pts',(2.71934892773146,2.275,-4.99536294016668E-16));
#19404=CARTESIAN_POINT('Ctrl Pts',(2.03951169579859,2.33333333333333,1.17751262658471));
#19405=CARTESIAN_POINT('Ctrl Pts',(1.35967446386573,2.39166666666666,2.35502525316942));
#19406=CARTESIAN_POINT('Ctrl Pts',(0.,2.45,2.35502525316942));
#19407=CARTESIAN_POINT('Ctrl Pts',(-1.35967446386573,2.50833333333333,2.35502525316942));
#19408=CARTESIAN_POINT('Ctrl Pts',(-2.03951169579859,2.56666666666666,1.17751262658471));
#19409=CARTESIAN_POINT('Ctrl Pts',(-2.71934892773146,2.62499999999999,1.66512098005556E-16));
#19410=CARTESIAN_POINT('Ctrl Pts',(-2.03951169579859,2.68333333333333,-1.17751262658471));
#19411=CARTESIAN_POINT('Ctrl Pts',(-1.35967446386573,2.74166666666666,-2.35502525316942));
#19412=CARTESIAN_POINT('Ctrl Pts',(-2.88407413820511E-16,2.8,-2.35502525316942));
#19413=CARTESIAN_POINT('Ctrl Pts',(1.35967446386573,2.85833333333333,-2.35502525316942));
#19414=CARTESIAN_POINT('Ctrl Pts',(2.03951169579859,2.91666666666666,-1.17751262658471));
#19415=CARTESIAN_POINT('Ctrl Pts',(2.71934892773146,2.97499999999999,-4.99536294016668E-16));
#19416=CARTESIAN_POINT('Ctrl Pts',(2.03951169579859,3.03333333333333,1.17751262658471));
#19417=CARTESIAN_POINT('Ctrl Pts',(1.35967446386573,3.09166666666666,2.35502525316942));
#19418=CARTESIAN_POINT('Ctrl Pts',(0.,3.14999999999999,2.35502525316942));
#19419=CARTESIAN_POINT('Ctrl Pts',(-1.35967446386573,3.20833333333333,2.35502525316942));
#19420=CARTESIAN_POINT('Ctrl Pts',(-2.03951169579859,3.26666666666666,1.17751262658471));
#19421=CARTESIAN_POINT('Ctrl Pts',(-2.71934892773146,3.32499999999999,1.66512098005556E-16));
#19422=CARTESIAN_POINT('Ctrl Pts',(-2.03951169579859,3.38333333333333,-1.17751262658471));
#19423=CARTESIAN_POINT('Ctrl Pts',(-1.35967446386573,3.44166666666666,-2.35502525316942));
#19424=CARTESIAN_POINT('Ctrl Pts',(-2.88407413820511E-16,3.49999999999999,
-2.35502525316942));
#19425=CARTESIAN_POINT('Ctrl Pts',(1.35967446386573,3.55833333333333,-2.35502525316942));
#19426=CARTESIAN_POINT('Ctrl Pts',(2.03951169579859,3.61666666666666,-1.17751262658471));
#19427=CARTESIAN_POINT('Ctrl Pts',(2.71934892773146,3.67499999999999,-4.99536294016668E-16));
#19428=CARTESIAN_POINT('Ctrl Pts',(2.03951169579859,3.73333333333333,1.17751262658471));
#19429=CARTESIAN_POINT('Ctrl Pts',(1.35967446386573,3.79166666666666,2.35502525316942));
#19430=CARTESIAN_POINT('Ctrl Pts',(0.,3.84999999999999,2.35502525316942));
#19431=CARTESIAN_POINT('Ctrl Pts',(-1.35967446386573,3.90833333333333,2.35502525316942));
#19432=CARTESIAN_POINT('Ctrl Pts',(-2.03951169579859,3.96666666666666,1.17751262658471));
#19433=CARTESIAN_POINT('Ctrl Pts',(-2.71934892773146,4.02499999999999,1.66512098005556E-16));
#19434=CARTESIAN_POINT('Ctrl Pts',(-2.03951169579859,4.08333333333333,-1.17751262658471));
#19435=CARTESIAN_POINT('Ctrl Pts',(-1.35967446386573,4.14166666666666,-2.35502525316942));
#19436=CARTESIAN_POINT('Ctrl Pts',(-2.88407413820511E-16,4.19999999999999,
-2.35502525316942));
#19437=CARTESIAN_POINT('Ctrl Pts',(1.35967446386573,4.25833333333332,-2.35502525316942));
#19438=CARTESIAN_POINT('Ctrl Pts',(2.03951169579859,4.31666666666666,-1.17751262658471));
#19439=CARTESIAN_POINT('Ctrl Pts',(2.71934892773146,4.37499999999999,-4.99536294016668E-16));
#19440=CARTESIAN_POINT('Ctrl Pts',(2.03951169579859,4.43333333333332,1.17751262658471));
#19441=CARTESIAN_POINT('Ctrl Pts',(1.35967446386573,4.49166666666666,2.35502525316942));
#19442=CARTESIAN_POINT('Ctrl Pts',(0.,4.54999999999999,2.35502525316942));
#19443=CARTESIAN_POINT('Ctrl Pts',(0.,0.205025253169417,2.5));
#19444=CARTESIAN_POINT('Ctrl Pts',(-1.44337567297406,0.26335858650275,2.5));
#19445=CARTESIAN_POINT('Ctrl Pts',(-2.1650635094611,0.321691919836083,1.25));
#19446=CARTESIAN_POINT('Ctrl Pts',(-2.88675134594813,0.380025253169416,
1.76762539787484E-16));
#19447=CARTESIAN_POINT('Ctrl Pts',(-2.1650635094611,0.43835858650275,-1.25));
#19448=CARTESIAN_POINT('Ctrl Pts',(-1.44337567297407,0.496691919836083,
-2.5));
#19449=CARTESIAN_POINT('Ctrl Pts',(-3.06161699786838E-16,0.555025253169416,
-2.5));
#19450=CARTESIAN_POINT('Ctrl Pts',(1.44337567297406,0.613358586502749,-2.5));
#19451=CARTESIAN_POINT('Ctrl Pts',(2.1650635094611,0.671691919836083,-1.25));
#19452=CARTESIAN_POINT('Ctrl Pts',(2.88675134594813,0.730025253169416,-5.30287619362453E-16));
#19453=CARTESIAN_POINT('Ctrl Pts',(2.1650635094611,0.788358586502749,1.25));
#19454=CARTESIAN_POINT('Ctrl Pts',(1.44337567297407,0.846691919836082,2.5));
#19455=CARTESIAN_POINT('Ctrl Pts',(0.,0.905025253169415,2.5));
#19456=CARTESIAN_POINT('Ctrl Pts',(-1.44337567297406,0.963358586502749,
2.5));
#19457=CARTESIAN_POINT('Ctrl Pts',(-2.1650635094611,1.02169191983608,1.25));
#19458=CARTESIAN_POINT('Ctrl Pts',(-2.88675134594813,1.08002525316942,1.76762539787484E-16));
#19459=CARTESIAN_POINT('Ctrl Pts',(-2.1650635094611,1.13835858650275,-1.25));
#19460=CARTESIAN_POINT('Ctrl Pts',(-1.44337567297407,1.19669191983608,-2.5));
#19461=CARTESIAN_POINT('Ctrl Pts',(-3.06161699786838E-16,1.25502525316941,
-2.5));
#19462=CARTESIAN_POINT('Ctrl Pts',(1.44337567297406,1.31335858650275,-2.5));
#19463=CARTESIAN_POINT('Ctrl Pts',(2.1650635094611,1.37169191983608,-1.25));
#19464=CARTESIAN_POINT('Ctrl Pts',(2.88675134594813,1.43002525316941,-5.30287619362453E-16));
#19465=CARTESIAN_POINT('Ctrl Pts',(2.1650635094611,1.48835858650275,1.25));
#19466=CARTESIAN_POINT('Ctrl Pts',(1.44337567297407,1.54669191983608,2.5));
#19467=CARTESIAN_POINT('Ctrl Pts',(0.,1.60502525316941,2.5));
#19468=CARTESIAN_POINT('Ctrl Pts',(-1.44337567297406,1.66335858650275,2.5));
#19469=CARTESIAN_POINT('Ctrl Pts',(-2.1650635094611,1.72169191983608,1.25));
#19470=CARTESIAN_POINT('Ctrl Pts',(-2.88675134594813,1.78002525316941,1.76762539787484E-16));
#19471=CARTESIAN_POINT('Ctrl Pts',(-2.1650635094611,1.83835858650275,-1.25));
#19472=CARTESIAN_POINT('Ctrl Pts',(-1.44337567297407,1.89669191983608,-2.5));
#19473=CARTESIAN_POINT('Ctrl Pts',(-3.06161699786838E-16,1.95502525316941,
-2.5));
#19474=CARTESIAN_POINT('Ctrl Pts',(1.44337567297406,2.01335858650275,-2.5));
#19475=CARTESIAN_POINT('Ctrl Pts',(2.1650635094611,2.07169191983608,-1.25));
#19476=CARTESIAN_POINT('Ctrl Pts',(2.88675134594813,2.13002525316941,-5.30287619362453E-16));
#19477=CARTESIAN_POINT('Ctrl Pts',(2.1650635094611,2.18835858650275,1.25));
#19478=CARTESIAN_POINT('Ctrl Pts',(1.44337567297407,2.24669191983608,2.5));
#19479=CARTESIAN_POINT('Ctrl Pts',(0.,2.30502525316941,2.5));
#19480=CARTESIAN_POINT('Ctrl Pts',(-1.44337567297406,2.36335858650275,2.5));
#19481=CARTESIAN_POINT('Ctrl Pts',(-2.1650635094611,2.42169191983608,1.25));
#19482=CARTESIAN_POINT('Ctrl Pts',(-2.88675134594813,2.48002525316941,1.76762539787484E-16));
#19483=CARTESIAN_POINT('Ctrl Pts',(-2.1650635094611,2.53835858650275,-1.25));
#19484=CARTESIAN_POINT('Ctrl Pts',(-1.44337567297407,2.59669191983608,-2.5));
#19485=CARTESIAN_POINT('Ctrl Pts',(-3.06161699786838E-16,2.65502525316941,
-2.5));
#19486=CARTESIAN_POINT('Ctrl Pts',(1.44337567297406,2.71335858650274,-2.5));
#19487=CARTESIAN_POINT('Ctrl Pts',(2.1650635094611,2.77169191983608,-1.25));
#19488=CARTESIAN_POINT('Ctrl Pts',(2.88675134594813,2.83002525316941,-5.30287619362453E-16));
#19489=CARTESIAN_POINT('Ctrl Pts',(2.1650635094611,2.88835858650274,1.25));
#19490=CARTESIAN_POINT('Ctrl Pts',(1.44337567297407,2.94669191983608,2.5));
#19491=CARTESIAN_POINT('Ctrl Pts',(0.,3.00502525316941,2.5));
#19492=CARTESIAN_POINT('Ctrl Pts',(-1.44337567297406,3.06335858650274,2.5));
#19493=CARTESIAN_POINT('Ctrl Pts',(-2.1650635094611,3.12169191983608,1.25));
#19494=CARTESIAN_POINT('Ctrl Pts',(-2.88675134594813,3.18002525316941,1.76762539787484E-16));
#19495=CARTESIAN_POINT('Ctrl Pts',(-2.1650635094611,3.23835858650274,-1.25));
#19496=CARTESIAN_POINT('Ctrl Pts',(-1.44337567297407,3.29669191983608,-2.5));
#19497=CARTESIAN_POINT('Ctrl Pts',(-3.06161699786838E-16,3.35502525316941,
-2.5));
#19498=CARTESIAN_POINT('Ctrl Pts',(1.44337567297406,3.41335858650274,-2.5));
#19499=CARTESIAN_POINT('Ctrl Pts',(2.1650635094611,3.47169191983608,-1.25));
#19500=CARTESIAN_POINT('Ctrl Pts',(2.88675134594813,3.53002525316941,-5.30287619362453E-16));
#19501=CARTESIAN_POINT('Ctrl Pts',(2.1650635094611,3.58835858650274,1.25));
#19502=CARTESIAN_POINT('Ctrl Pts',(1.44337567297407,3.64669191983608,2.5));
#19503=CARTESIAN_POINT('Ctrl Pts',(0.,3.70502525316941,2.5));
#19504=CARTESIAN_POINT('Ctrl Pts',(-1.44337567297406,3.76335858650274,2.5));
#19505=CARTESIAN_POINT('Ctrl Pts',(-2.1650635094611,3.82169191983608,1.25));
#19506=CARTESIAN_POINT('Ctrl Pts',(-2.88675134594813,3.88002525316941,1.76762539787484E-16));
#19507=CARTESIAN_POINT('Ctrl Pts',(-2.1650635094611,3.93835858650274,-1.25));
#19508=CARTESIAN_POINT('Ctrl Pts',(-1.44337567297407,3.99669191983608,-2.5));
#19509=CARTESIAN_POINT('Ctrl Pts',(-3.06161699786838E-16,4.05502525316941,
-2.5));
#19510=CARTESIAN_POINT('Ctrl Pts',(1.44337567297406,4.11335858650274,-2.5));
#19511=CARTESIAN_POINT('Ctrl Pts',(2.1650635094611,4.17169191983608,-1.25));
#19512=CARTESIAN_POINT('Ctrl Pts',(2.88675134594813,4.23002525316941,-5.30287619362453E-16));
#19513=CARTESIAN_POINT('Ctrl Pts',(2.1650635094611,4.28835858650274,1.25));
#19514=CARTESIAN_POINT('Ctrl Pts',(1.44337567297407,4.34669191983608,2.5));
#19515=CARTESIAN_POINT('Ctrl Pts',(0.,4.40502525316941,2.5));
#19516=CARTESIAN_POINT('Ctrl Pts',(0.,4.28626379701574E-17,2.5));
#19517=CARTESIAN_POINT('Ctrl Pts',(-1.44337567297406,0.0583333333333333,
2.5));
#19518=CARTESIAN_POINT('Ctrl Pts',(-2.1650635094611,0.116666666666666,1.25));
#19519=CARTESIAN_POINT('Ctrl Pts',(-2.88675134594813,0.175,1.76762539787484E-16));
#19520=CARTESIAN_POINT('Ctrl Pts',(-2.1650635094611,0.233333333333333,-1.25));
#19521=CARTESIAN_POINT('Ctrl Pts',(-1.44337567297407,0.291666666666666,
-2.5));
#19522=CARTESIAN_POINT('Ctrl Pts',(-3.06161699786838E-16,0.349999999999999,
-2.5));
#19523=CARTESIAN_POINT('Ctrl Pts',(1.44337567297406,0.408333333333333,-2.5));
#19524=CARTESIAN_POINT('Ctrl Pts',(2.1650635094611,0.466666666666666,-1.25));
#19525=CARTESIAN_POINT('Ctrl Pts',(2.88675134594813,0.524999999999999,-5.30287619362453E-16));
#19526=CARTESIAN_POINT('Ctrl Pts',(2.1650635094611,0.583333333333332,1.25));
#19527=CARTESIAN_POINT('Ctrl Pts',(1.44337567297407,0.641666666666665,2.5));
#19528=CARTESIAN_POINT('Ctrl Pts',(0.,0.699999999999999,2.5));
#19529=CARTESIAN_POINT('Ctrl Pts',(-1.44337567297406,0.758333333333332,
2.5));
#19530=CARTESIAN_POINT('Ctrl Pts',(-2.1650635094611,0.816666666666665,1.25));
#19531=CARTESIAN_POINT('Ctrl Pts',(-2.88675134594813,0.874999999999998,
1.76762539787484E-16));
#19532=CARTESIAN_POINT('Ctrl Pts',(-2.1650635094611,0.933333333333332,-1.25));
#19533=CARTESIAN_POINT('Ctrl Pts',(-1.44337567297407,0.991666666666665,
-2.5));
#19534=CARTESIAN_POINT('Ctrl Pts',(-3.06161699786838E-16,1.05,-2.5));
#19535=CARTESIAN_POINT('Ctrl Pts',(1.44337567297406,1.10833333333333,-2.5));
#19536=CARTESIAN_POINT('Ctrl Pts',(2.1650635094611,1.16666666666666,-1.25));
#19537=CARTESIAN_POINT('Ctrl Pts',(2.88675134594813,1.225,-5.30287619362453E-16));
#19538=CARTESIAN_POINT('Ctrl Pts',(2.1650635094611,1.28333333333333,1.25));
#19539=CARTESIAN_POINT('Ctrl Pts',(1.44337567297407,1.34166666666666,2.5));
#19540=CARTESIAN_POINT('Ctrl Pts',(0.,1.4,2.5));
#19541=CARTESIAN_POINT('Ctrl Pts',(-1.44337567297406,1.45833333333333,2.5));
#19542=CARTESIAN_POINT('Ctrl Pts',(-2.1650635094611,1.51666666666666,1.25));
#19543=CARTESIAN_POINT('Ctrl Pts',(-2.88675134594813,1.575,1.76762539787484E-16));
#19544=CARTESIAN_POINT('Ctrl Pts',(-2.1650635094611,1.63333333333333,-1.25));
#19545=CARTESIAN_POINT('Ctrl Pts',(-1.44337567297407,1.69166666666666,-2.5));
#19546=CARTESIAN_POINT('Ctrl Pts',(-3.06161699786838E-16,1.75,-2.5));
#19547=CARTESIAN_POINT('Ctrl Pts',(1.44337567297406,1.80833333333333,-2.5));
#19548=CARTESIAN_POINT('Ctrl Pts',(2.1650635094611,1.86666666666666,-1.25));
#19549=CARTESIAN_POINT('Ctrl Pts',(2.88675134594813,1.925,-5.30287619362453E-16));
#19550=CARTESIAN_POINT('Ctrl Pts',(2.1650635094611,1.98333333333333,1.25));
#19551=CARTESIAN_POINT('Ctrl Pts',(1.44337567297407,2.04166666666666,2.5));
#19552=CARTESIAN_POINT('Ctrl Pts',(0.,2.1,2.5));
#19553=CARTESIAN_POINT('Ctrl Pts',(-1.44337567297406,2.15833333333333,2.5));
#19554=CARTESIAN_POINT('Ctrl Pts',(-2.1650635094611,2.21666666666666,1.25));
#19555=CARTESIAN_POINT('Ctrl Pts',(-2.88675134594813,2.275,1.76762539787484E-16));
#19556=CARTESIAN_POINT('Ctrl Pts',(-2.1650635094611,2.33333333333333,-1.25));
#19557=CARTESIAN_POINT('Ctrl Pts',(-1.44337567297407,2.39166666666666,-2.5));
#19558=CARTESIAN_POINT('Ctrl Pts',(-3.06161699786838E-16,2.45,-2.5));
#19559=CARTESIAN_POINT('Ctrl Pts',(1.44337567297406,2.50833333333333,-2.5));
#19560=CARTESIAN_POINT('Ctrl Pts',(2.1650635094611,2.56666666666666,-1.25));
#19561=CARTESIAN_POINT('Ctrl Pts',(2.88675134594813,2.62499999999999,-5.30287619362453E-16));
#19562=CARTESIAN_POINT('Ctrl Pts',(2.1650635094611,2.68333333333333,1.25));
#19563=CARTESIAN_POINT('Ctrl Pts',(1.44337567297407,2.74166666666666,2.5));
#19564=CARTESIAN_POINT('Ctrl Pts',(0.,2.79999999999999,2.5));
#19565=CARTESIAN_POINT('Ctrl Pts',(-1.44337567297406,2.85833333333333,2.5));
#19566=CARTESIAN_POINT('Ctrl Pts',(-2.1650635094611,2.91666666666666,1.25));
#19567=CARTESIAN_POINT('Ctrl Pts',(-2.88675134594813,2.97499999999999,1.76762539787484E-16));
#19568=CARTESIAN_POINT('Ctrl Pts',(-2.1650635094611,3.03333333333333,-1.25));
#19569=CARTESIAN_POINT('Ctrl Pts',(-1.44337567297407,3.09166666666666,-2.5));
#19570=CARTESIAN_POINT('Ctrl Pts',(-3.06161699786838E-16,3.14999999999999,
-2.5));
#19571=CARTESIAN_POINT('Ctrl Pts',(1.44337567297406,3.20833333333333,-2.5));
#19572=CARTESIAN_POINT('Ctrl Pts',(2.1650635094611,3.26666666666666,-1.25));
#19573=CARTESIAN_POINT('Ctrl Pts',(2.88675134594813,3.32499999999999,-5.30287619362453E-16));
#19574=CARTESIAN_POINT('Ctrl Pts',(2.1650635094611,3.38333333333333,1.25));
#19575=CARTESIAN_POINT('Ctrl Pts',(1.44337567297407,3.44166666666666,2.5));
#19576=CARTESIAN_POINT('Ctrl Pts',(0.,3.49999999999999,2.5));
#19577=CARTESIAN_POINT('Ctrl Pts',(-1.44337567297406,3.55833333333333,2.5));
#19578=CARTESIAN_POINT('Ctrl Pts',(-2.1650635094611,3.61666666666666,1.25));
#19579=CARTESIAN_POINT('Ctrl Pts',(-2.88675134594813,3.67499999999999,1.76762539787484E-16));
#19580=CARTESIAN_POINT('Ctrl Pts',(-2.1650635094611,3.73333333333333,-1.25));
#19581=CARTESIAN_POINT('Ctrl Pts',(-1.44337567297407,3.79166666666666,-2.5));
#19582=CARTESIAN_POINT('Ctrl Pts',(-3.06161699786838E-16,3.84999999999999,
-2.5));
#19583=CARTESIAN_POINT('Ctrl Pts',(1.44337567297406,3.90833333333333,-2.5));
#19584=CARTESIAN_POINT('Ctrl Pts',(2.1650635094611,3.96666666666666,-1.25));
#19585=CARTESIAN_POINT('Ctrl Pts',(2.88675134594813,4.02499999999999,-5.30287619362453E-16));
#19586=CARTESIAN_POINT('Ctrl Pts',(2.1650635094611,4.08333333333333,1.25));
#19587=CARTESIAN_POINT('Ctrl Pts',(1.44337567297407,4.14166666666666,2.5));
#19588=CARTESIAN_POINT('Ctrl Pts',(0.,4.19999999999999,2.5));
#19589=CARTESIAN_POINT('Origin',(0.,0.,2.15));
#19590=CARTESIAN_POINT('Origin',(-1.80160437084306E-13,4.2,2.15));
#19591=CARTESIAN_POINT('Origin',(-1.80160437084306E-13,4.2,2.15));
#19592=CARTESIAN_POINT('Origin',(0.,0.,2.15));
#32960=UNCERTAINTY_MEASURE_WITH_UNIT(LENGTH_MEASURE(0.01),#33017,
'DISTANCE_ACCURACY_VALUE',
'Maximum model space distance between geometric entities at asserted c
onnectivities');
#32984=UNCERTAINTY_MEASURE_WITH_UNIT(LENGTH_MEASURE(0.01),#33017,
'DISTANCE_ACCURACY_VALUE',
'Maximum model space distance between geometric entities at asserted c
onnectivities');
#32992=(
GEOMETRIC_REPRESENTATION_CONTEXT(3)
GLOBAL_UNCERTAINTY_ASSIGNED_CONTEXT((#32960))
GLOBAL_UNIT_ASSIGNED_CONTEXT((#33017,#33019,#33020))
REPRESENTATION_CONTEXT('','3D')
);
#33016=(
GEOMETRIC_REPRESENTATION_CONTEXT(3)
GLOBAL_UNCERTAINTY_ASSIGNED_CONTEXT((#32984))
GLOBAL_UNIT_ASSIGNED_CONTEXT((#33017,#33019,#33020))
REPRESENTATION_CONTEXT('','3D')
);
#33017=(
LENGTH_UNIT()
NAMED_UNIT(*)
SI_UNIT(.MILLI.,.METRE.)
);
#33019=(
NAMED_UNIT(*)
PLANE_ANGLE_UNIT()
SI_UNIT($,.RADIAN.)
);
#33020=(
NAMED_UNIT(*)
SI_UNIT($,.STERADIAN.)
SOLID_ANGLE_UNIT()
);
#33028=SHAPE_DEFINITION_REPRESENTATION(#33059,#33131);
#33059=PRODUCT_DEFINITION_SHAPE('',$,#33163);
#33131=SHAPE_REPRESENTATION('',(#10666),#32992);
#33155=PRODUCT_DEFINITION_CONTEXT('part definition',#33250,'design');
#33163=PRODUCT_DEFINITION(
'BO21-002_Spring_PUR-HW-4007_0.7x5x6_M_Rev00 (C)','PUR-HW-4007',#33194,
#33155);
#33194=PRODUCT_DEFINITION_FORMATION('',$,#33259);
#33250=APPLICATION_CONTEXT(
'Core Data for Automotive Mechanical Design Process');
#33251=PRODUCT_CONTEXT('part definition',#33250,'mechanical');
#33259=PRODUCT('BO21-002_Spring_PUR-HW-4007_0.7x5x6_M_Rev00 (C)',
'PUR-HW-4007',$,(#33251));
#33285=PRESENTATION_STYLE_ASSIGNMENT((#33292));
#33292=SURFACE_STYLE_USAGE(.BOTH.,#33299);
#33299=SURFACE_SIDE_STYLE('',(#33306));
#33306=SURFACE_STYLE_FILL_AREA(#33313);
#33313=FILL_AREA_STYLE('Opaque(202,209,238)',(#33320));
#33320=FILL_AREA_STYLE_COLOUR('Opaque(202,209,238)',#33327);
#33327=COLOUR_RGB('Opaque(202,209,238)', 0.08235294, 0.09019608, 0.10196078);
ENDSEC;
END-ISO-10303-21;
